ISO-10303-21;
HEADER;
FILE_DESCRIPTION (('STEP AP214'),
    '1' );
FILE_NAME ('instrument roller bearing_iso_ISO 1224 - 171015 - R,24,SI,NC,24.step',
    '2026-09-30T13:58:28',
    ( '' ),
    ( '' ),
    'SwSTEP 2.0',
    'SolidWorks 2026',
    '' );
FILE_SCHEMA (( 'AUTOMOTIVE_DESIGN' ));
ENDSEC;

DATA;
#3=ORIENTED_EDGE ( 'NONE', *, *, #13016, .T. ) ;
#30=DIRECTION ( 'NONE',  ( 1.000000000000000000, 0.000000000000000000, 0.000000000000000000 ) ) ;
#39=ORIENTED_EDGE ( 'NONE', *, *, #420, .F. ) ;
#40=ADVANCED_FACE ( 'NONE', ( #13087 ), #18195, .T. ) ;
#76=ORIENTED_EDGE ( 'NONE', *, *, #8491, .T. ) ;
#86=DIRECTION ( 'NONE',  ( 1.000000000000000000, 0.000000000000000000, 0.000000000000000000 ) ) ;
#112=FACE_OUTER_BOUND ( 'NONE', #11461, .T. ) ;
#134=CIRCLE ( 'NONE', #12473, 5.100000000000000533 ) ;
#159=CARTESIAN_POINT ( 'NONE',  ( -1.500000000000001332, 0.000000000000000000, 0.000000000000000000 ) ) ;
#169=DIRECTION ( 'NONE',  ( 1.000000000000000000, 0.000000000000000000, 0.000000000000000000 ) ) ;
#172=AXIS2_PLACEMENT_3D ( 'NONE', #13423, #20277, #18409 ) ;
#190=EDGE_LOOP ( 'NONE', ( #15961, #11977 ) ) ;
#213=DIRECTION ( 'NONE',  ( 1.000000000000000000, 0.000000000000000000, 0.000000000000000000 ) ) ;
#217=ORIENTED_EDGE ( 'NONE', *, *, #17217, .F. ) ;
#247=DIRECTION ( 'NONE',  ( 1.000000000000000000, 0.000000000000000000, 0.000000000000000000 ) ) ;
#248=EDGE_CURVE ( 'NONE', #18258, #6557, #15949, .T. ) ;
#250=CARTESIAN_POINT ( 'NONE',  ( 1.500000000000001332, 0.000000000000000000, 0.000000000000000000 ) ) ;
#273=CIRCLE ( 'NONE', #3803, 5.000000000000000000 ) ;
#288=EDGE_CURVE ( 'NONE', #3210, #16203, #21321, .T. ) ;
#295=CIRCLE ( 'NONE', #15093, 7.500000000000021316 ) ;
#313=CARTESIAN_POINT ( 'NONE',  ( -1.400000000000000577, 0.000000000000000000, -7.400000000000019895 ) ) ;
#336=DIRECTION ( 'NONE',  ( 1.000000000000000000, 0.000000000000000000, 0.000000000000000000 ) ) ;
#341=DIRECTION ( 'NONE',  ( 1.000000000000000000, 0.000000000000000000, 0.000000000000000000 ) ) ;
#375=( NAMED_UNIT ( * ) PLANE_ANGLE_UNIT ( ) SI_UNIT ( $, .RADIAN. ) );
#397=DIRECTION ( 'NONE',  ( 0.000000000000000000, 0.000000000000000000, -1.000000000000000000 ) ) ;
#417=DIRECTION ( 'NONE',  ( 0.000000000000000000, 0.000000000000000000, -1.000000000000000000 ) ) ;
#420=EDGE_CURVE ( 'NONE', #17054, #16203, #9590, .T. ) ;
#452=EDGE_CURVE ( 'NONE', #3829, #10685, #18573, .T. ) ;
#465=ADVANCED_FACE ( 'NONE', ( #3425 ), #3311, .T. ) ;
#470=CIRCLE ( 'NONE', #16293, 5.612499999999999822 ) ;
#478=ORIENTED_EDGE ( 'NONE', *, *, #17582, .T. ) ;
#499=TOROIDAL_SURFACE ( 'NONE', #15302, 5.633200000000004870, 0.02570000000000143697 ) ;
#530=DIRECTION ( 'NONE',  ( 0.000000000000000000, 0.000000000000000000, -1.000000000000000000 ) ) ;
#539=DIRECTION ( 'NONE',  ( 0.000000000000000000, 0.000000000000000000, -1.000000000000000000 ) ) ;
#606=ORIENTED_EDGE ( 'NONE', *, *, #10944, .F. ) ;
#620=LINE ( 'NONE', #11105, #13677 ) ;
#631=AXIS2_PLACEMENT_3D ( 'NONE', #19053, #12308, #16964 ) ;
#656=DIRECTION ( 'NONE',  ( 0.000000000000000000, 0.000000000000000000, -1.000000000000000000 ) ) ;
#668=FACE_BOUND ( 'NONE', #13244, .T. ) ;
#712=EDGE_CURVE ( 'NONE', #14549, #21211, #470, .T. ) ;
#745=CARTESIAN_POINT ( 'NONE',  ( -1.200000000000000844, 6.887500000000022382, 0.000000000000000000 ) ) ;
#755=DIRECTION ( 'NONE',  ( 1.000000000000000000, -0.000000000000000000, -0.000000000000000000 ) ) ;
#769=VERTEX_POINT ( 'NONE', #21088 ) ;
#772=DIRECTION ( 'NONE',  ( 0.000000000000000000, 0.000000000000000000, -1.000000000000000000 ) ) ;
#774=APPLICATION_CONTEXT ( 'automotive_design' ) ;
#822=TOROIDAL_SURFACE ( 'NONE', #18833, 7.400000000000020783, 0.1000000000000001582 ) ;
#826=VERTEX_POINT ( 'NONE', #6509 ) ;
#928=AXIS2_PLACEMENT_3D ( 'NONE', #10346, #4045, #12341 ) ;
#930=FILL_AREA_STYLE ('',( #16181 ) ) ;
#932=EDGE_LOOP ( 'NONE', ( #20151, #4122, #12521, #8046 ) ) ;
#938=ORIENTED_EDGE ( 'NONE', *, *, #20300, .T. ) ;
#948=CIRCLE ( 'NONE', #1648, 0.1000000000000002554 ) ;
#955=ADVANCED_FACE ( 'NONE', ( #21532 ), #6409, .F. ) ;
#957=EDGE_CURVE ( 'NONE', #20241, #20636, #5718, .T. ) ;
#984=DIRECTION ( 'NONE',  ( 1.000000000000000000, 0.000000000000000000, 0.000000000000000000 ) ) ;
#1004=DIRECTION ( 'NONE',  ( 1.000000000000000000, -0.000000000000000000, -0.000000000000000000 ) ) ;
#1013=AXIS2_PLACEMENT_3D ( 'NONE', #21234, #8600, #16784 ) ;
#1043=CIRCLE ( 'NONE', #7406, 0.09999999999999939493 ) ;
#1049=CARTESIAN_POINT ( 'NONE',  ( -1.200000000000006617, 6.873330160214519262E-16, 5.612499999999999822 ) ) ;
#1054=VERTEX_POINT ( 'NONE', #20843 ) ;
#1085=CARTESIAN_POINT ( 'NONE',  ( -90.00000000000000000, 0.000000000000000000, 0.000000000000000000 ) ) ;
#1103=EDGE_CURVE ( 'NONE', #13440, #5078, #15091, .T. ) ;
#1116=COLOUR_RGB ( '', 0.31764706, 0.68627451, 0.89019608) ;
#1117=ORIENTED_EDGE ( 'NONE', *, *, #8904, .T. ) ;
#1128=VERTEX_POINT ( 'NONE', #9123 ) ;
#1152=( LENGTH_UNIT ( ) NAMED_UNIT ( * ) SI_UNIT ( .MILLI., .METRE. ) );
#1162=DIRECTION ( 'NONE',  ( 1.000000000000000000, 0.000000000000000000, 0.000000000000000000 ) ) ;
#1235=DIRECTION ( 'NONE',  ( 0.000000000000000000, 1.000000000000000000, -1.224646799147353207E-16 ) ) ;
#1242=ORIENTED_EDGE ( 'NONE', *, *, #288, .F. ) ;
#1294=DIRECTION ( 'NONE',  ( 0.000000000000000000, 0.000000000000000000, -1.000000000000000000 ) ) ;
#1304=CIRCLE ( 'NONE', #7298, 6.728125000000023448 ) ;
#1308=VERTEX_POINT ( 'NONE', #2928 ) ;
#1320=DIRECTION ( 'NONE',  ( 1.000000000000000000, 0.000000000000000000, 0.000000000000000000 ) ) ;
#1335=FACE_OUTER_BOUND ( 'NONE', #8331, .T. ) ;
#1340=EDGE_LOOP ( 'NONE', ( #11547, #938, #11995, #19443 ) ) ;
#1354=CYLINDRICAL_SURFACE ( 'NONE', #21447, 5.612499999999999822 ) ;
#1368=DIRECTION ( 'NONE',  ( -1.000000000000000000, 0.000000000000000000, 0.000000000000000000 ) ) ;
#1384=AXIS2_PLACEMENT_3D ( 'NONE', #16117, #984, #17782 ) ;
#1407=DIRECTION ( 'NONE',  ( 1.000000000000000000, 0.000000000000000000, 0.000000000000000000 ) ) ;
#1416=ORIENTED_EDGE ( 'NONE', *, *, #7888, .F. ) ;
#1472=EDGE_CURVE ( 'NONE', #6262, #13819, #16119, .T. ) ;
#1479=CARTESIAN_POINT ( 'NONE',  ( 1.129531546211678616, 0.000000000000000000, 0.000000000000000000 ) ) ;
#1480=ORIENTED_EDGE ( 'NONE', *, *, #4866, .T. ) ;
#1482=CARTESIAN_POINT ( 'NONE',  ( 1.399999999999999245, 0.000000000000000000, -7.400000000000020783 ) ) ;
#1485=ADVANCED_FACE ( 'NONE', ( #20388 ), #10859, .T. ) ;
#1515=LINE ( 'NONE', #7821, #8632 ) ;
#1524=AXIS2_PLACEMENT_3D ( 'NONE', #10527, #14164, #20907 ) ;
#1530=CIRCLE ( 'NONE', #16337, 5.000000000000000888 ) ;
#1556=CARTESIAN_POINT ( 'NONE',  ( 1.500000000000001332, 0.000000000000000000, 0.000000000000000000 ) ) ;
#1567=CARTESIAN_POINT ( 'NONE',  ( -90.00000000000000000, 0.000000000000000000, 0.000000000000000000 ) ) ;
#1570=CIRCLE ( 'NONE', #12149, 6.887500000000022382 ) ;
#1589=ORIENTED_EDGE ( 'NONE', *, *, #12560, .F. ) ;
#1591=FACE_OUTER_BOUND ( 'NONE', #14853, .T. ) ;
#1600=AXIS2_PLACEMENT_3D ( 'NONE', #21822, #1718, #11556 ) ;
#1621=DIRECTION ( 'NONE',  ( 1.000000000000000000, 0.000000000000000000, 0.000000000000000000 ) ) ;
#1630=EDGE_LOOP ( 'NONE', ( #3742, #9026, #11606, #14649 ) ) ;
#1648=AXIS2_PLACEMENT_3D ( 'NONE', #10143, #11361, #13127 ) ;
#1653=ORIENTED_EDGE ( 'NONE', *, *, #4765, .T. ) ;
#1709=ORIENTED_EDGE ( 'NONE', *, *, #6273, .T. ) ;
#1712=DIRECTION ( 'NONE',  ( 1.000000000000000000, 0.000000000000000000, 0.000000000000000000 ) ) ;
#1718=DIRECTION ( 'NONE',  ( 0.000000000000000000, 1.000000000000000000, -1.224646799147353207E-16 ) ) ;
#1736=ORIENTED_EDGE ( 'NONE', *, *, #12188, .T. ) ;
#1738=EDGE_LOOP ( 'NONE', ( #4235, #16570, #14554, #8920 ) ) ;
#1748=EDGE_CURVE ( 'NONE', #1308, #12422, #19169, .T. ) ;
#1767=DIRECTION ( 'NONE',  ( 1.000000000000000000, 0.000000000000000000, 0.000000000000000000 ) ) ;
#1809=ADVANCED_FACE ( 'NONE', ( #4896 ), #12463, .T. ) ;
#1810=ORIENTED_EDGE ( 'NONE', *, *, #13767, .T. ) ;
#1855=DIRECTION ( 'NONE',  ( 0.000000000000000000, 0.000000000000000000, -1.000000000000000000 ) ) ;
#1867=ORIENTED_EDGE ( 'NONE', *, *, #18226, .T. ) ;
#1875=CARTESIAN_POINT ( 'NONE',  ( -1.114300000000000290, 0.000000000000000000, 0.000000000000000000 ) ) ;
#1881=ORIENTED_EDGE ( 'NONE', *, *, #11741, .T. ) ;
#1923=DIRECTION ( 'NONE',  ( 0.000000000000000000, 0.000000000000000000, -1.000000000000000000 ) ) ;
#1945=CARTESIAN_POINT ( 'NONE',  ( -90.00000000000000000, 0.000000000000000000, 0.000000000000000000 ) ) ;
#1952=DIRECTION ( 'NONE',  ( 0.000000000000000000, 0.000000000000000000, -1.000000000000000000 ) ) ;
#1983=DIRECTION ( 'NONE',  ( -1.000000000000000000, 0.000000000000000000, -0.000000000000000000 ) ) ;
#2012=CARTESIAN_POINT ( 'NONE',  ( -1.200000000000006617, 0.000000000000000000, 0.000000000000000000 ) ) ;
#2033=CARTESIAN_POINT ( 'NONE',  ( 1.399999999999999245, 9.062386313690440012E-16, 7.400000000000020783 ) ) ;
#2059=CIRCLE ( 'NONE', #12981, 7.400000000000019895 ) ;
#2083=FACE_OUTER_BOUND ( 'NONE', #20750, .T. ) ;
#2086=DIRECTION ( 'NONE',  ( 0.000000000000000000, 1.000000000000000000, -1.224646799147353207E-16 ) ) ;
#2148=DIRECTION ( 'NONE',  ( 0.000000000000000000, 0.000000000000000000, -1.000000000000000000 ) ) ;
#2156=FACE_OUTER_BOUND ( 'NONE', #2680, .T. ) ;
#2170=DIRECTION ( 'NONE',  ( 0.000000000000000000, 0.000000000000000000, -1.000000000000000000 ) ) ;
#2178=DIRECTION ( 'NONE',  ( -1.000000000000000000, -0.000000000000000000, -0.000000000000000000 ) ) ;
#2201=ORIENTED_EDGE ( 'NONE', *, *, #16501, .F. ) ;
#2203=DIRECTION ( 'NONE',  ( 1.000000000000000000, 0.000000000000000000, 0.000000000000000000 ) ) ;
#2217=EDGE_LOOP ( 'NONE', ( #2814, #18602, #478, #11703 ) ) ;
#2226=DIRECTION ( 'NONE',  ( 0.000000000000000000, 0.000000000000000000, -1.000000000000000000 ) ) ;
#2230=CIRCLE ( 'NONE', #16331, 6.887500000000022382 ) ;
#2233=AXIS2_PLACEMENT_3D ( 'NONE', #1085, #9245, #6180 ) ;
#2247=DIRECTION ( 'NONE',  ( 0.000000000000000000, 1.000000000000000000, -1.224646799147353207E-16 ) ) ;
#2258=CARTESIAN_POINT ( 'NONE',  ( 1.399999999999998579, 9.184850993605177527E-16, 7.500000000000022204 ) ) ;
#2273=CARTESIAN_POINT ( 'NONE',  ( -1.200000000000006617, 0.000000000000000000, -6.728125000000022560 ) ) ;
#2281=EDGE_CURVE ( 'NONE', #1054, #6321, #8703, .T. ) ;
#2301=CARTESIAN_POINT ( 'NONE',  ( -90.00000000000000000, 8.434754829127421589E-16, 6.887500000000022382 ) ) ;
#2332=FACE_OUTER_BOUND ( 'NONE', #3263, .T. ) ;
#2363=TOROIDAL_SURFACE ( 'NONE', #18246, 6.866799999999992465, 0.02570000000000154800 ) ;
#2391=EDGE_CURVE ( 'NONE', #6398, #12588, #5257, .T. ) ;
#2461=CARTESIAN_POINT ( 'NONE',  ( -1.114300000000000068, 0.000000000000000000, -5.633200000000004870 ) ) ;
#2508=CARTESIAN_POINT ( 'NONE',  ( 1.400000000000000133, 0.000000000000000000, 0.000000000000000000 ) ) ;
#2519=STYLED_ITEM ( 'NONE', ( #12189 ), #4298 ) ;
#2562=VERTEX_POINT ( 'NONE', #20282 ) ;
#2576=DIRECTION ( 'NONE',  ( 1.000000000000000000, 0.000000000000000000, 0.000000000000000000 ) ) ;
#2580=AXIS2_PLACEMENT_3D ( 'NONE', #8266, #9683, #6410 ) ;
#2582=LINE ( 'NONE', #1049, #12961 ) ;
#2585=CARTESIAN_POINT ( 'NONE',  ( -90.00000000000000000, 0.000000000000000000, 0.000000000000000000 ) ) ;
#2592=ORIENTED_EDGE ( 'NONE', *, *, #14205, .T. ) ;
#2635=FACE_OUTER_BOUND ( 'NONE', #18479, .T. ) ;
#2656=ADVANCED_FACE ( 'NONE', ( #15078 ), #21825, .F. ) ;
#2680=EDGE_LOOP ( 'NONE', ( #8458, #4593, #12132, #11621 ) ) ;
#2682=DIRECTION ( 'NONE',  ( 0.000000000000000000, 0.000000000000000000, -1.000000000000000000 ) ) ;
#2706=LINE ( 'NONE', #4809, #16007 ) ;
#2764=EDGE_LOOP ( 'NONE', ( #4176, #1480, #20463, #16420 ) ) ;
#2776=CARTESIAN_POINT ( 'NONE',  ( -90.00000000000000000, 6.873330160214519262E-16, 5.612499999999999822 ) ) ;
#2814=ORIENTED_EDGE ( 'NONE', *, *, #18781, .F. ) ;
#2816=AXIS2_PLACEMENT_3D ( 'NONE', #9896, #5153, #7028 ) ;
#2842=ADVANCED_FACE ( 'NONE', ( #4245 ), #8041, .T. ) ;
#2844=CIRCLE ( 'NONE', #4976, 5.453125000000000000 ) ;
#2888=AXIS2_PLACEMENT_3D ( 'NONE', #4841, #11582, #3287 ) ;
#2914=( NAMED_UNIT ( * ) SI_UNIT ( $, .STERADIAN. ) SOLID_ANGLE_UNIT ( ) );
#2928=CARTESIAN_POINT ( 'NONE',  ( -1.200000000000006617, 8.239576745513313235E-16, 6.728125000000022560 ) ) ;
#2944=LINE ( 'NONE', #8249, #10912 ) ;
#2950=EDGE_LOOP ( 'NONE', ( #16762, #1736 ) ) ;
#2967=DIRECTION ( 'NONE',  ( 1.000000000000000000, 0.000000000000000000, 0.000000000000000000 ) ) ;
#2971=ORIENTED_EDGE ( 'NONE', *, *, #17539, .F. ) ;
#2979=CIRCLE ( 'NONE', #14671, 6.866799999999992465 ) ;
#2991=ORIENTED_EDGE ( 'NONE', *, *, #4765, .F. ) ;
#3031=ORIENTED_EDGE ( 'NONE', *, *, #2391, .F. ) ;
#3062=DIRECTION ( 'NONE',  ( 0.000000000000000000, 0.000000000000000000, -1.000000000000000000 ) ) ;
#3073=CARTESIAN_POINT ( 'NONE',  ( 1.139999999999997460, 5.633200000000004870, 0.000000000000000000 ) ) ;
#3105=DIRECTION ( 'NONE',  ( 1.000000000000000000, 0.000000000000000000, 0.000000000000000000 ) ) ;
#3135=ADVANCED_FACE ( 'NONE', ( #10512 ), #16031, .T. ) ;
#3149=DIRECTION ( 'NONE',  ( 1.000000000000000000, 0.000000000000000000, 0.000000000000000000 ) ) ;
#3187=CARTESIAN_POINT ( 'NONE',  ( -1.400000000000000577, 0.000000000000000000, 0.000000000000000000 ) ) ;
#3210=VERTEX_POINT ( 'NONE', #15597 ) ;
#3227=DIRECTION ( 'NONE',  ( 1.000000000000000000, 0.000000000000000000, 0.000000000000000000 ) ) ;
#3261=UNCERTAINTY_MEASURE_WITH_UNIT (LENGTH_MEASURE( 1.000000000000000082E-05 ), #9086, 'distance_accuracy_value', 'NONE');
#3263=EDGE_LOOP ( 'NONE', ( #9431, #5750, #15890, #9883 ) ) ;
#3287=DIRECTION ( 'NONE',  ( 0.000000000000000000, 0.000000000000000000, -1.000000000000000000 ) ) ;
#3291=AXIS2_PLACEMENT_3D ( 'NONE', #8834, #341, #7401 ) ;
#3311=CYLINDRICAL_SURFACE ( 'NONE', #3617, 5.612499999999999822 ) ;
#3359=AXIS2_PLACEMENT_3D ( 'NONE', #15552, #18666, #417 ) ;
#3391=EDGE_LOOP ( 'NONE', ( #7631, #17168 ) ) ;
#3413=EDGE_LOOP ( 'NONE', ( #10496, #1416, #20055, #4198 ) ) ;
#3422=CARTESIAN_POINT ( 'NONE',  ( -90.00000000000000000, 0.000000000000000000, 0.000000000000000000 ) ) ;
#3425=FACE_OUTER_BOUND ( 'NONE', #8342, .T. ) ;
#3466=VERTEX_POINT ( 'NONE', #16583 ) ;
#3483=CARTESIAN_POINT ( 'NONE',  ( -1.500000000000001332, 0.000000000000000000, -7.400000000000019895 ) ) ;
#3484=CARTESIAN_POINT ( 'NONE',  ( -1.399999999999998579, 0.000000000000000000, 0.000000000000000000 ) ) ;
#3491=AXIS2_PLACEMENT_3D ( 'NONE', #9136, #15889, #7489 ) ;
#3529=ORIENTED_EDGE ( 'NONE', *, *, #4313, .F. ) ;
#3546=ADVANCED_FACE ( 'NONE', ( #112 ), #2363, .T. ) ;
#3575=DIRECTION ( 'NONE',  ( 1.000000000000000000, -0.000000000000000000, -0.000000000000000000 ) ) ;
#3582=( GEOMETRIC_REPRESENTATION_CONTEXT ( 3 ) GLOBAL_UNCERTAINTY_ASSIGNED_CONTEXT ( ( #3261 ) ) GLOBAL_UNIT_ASSIGNED_CONTEXT ( ( #9086, #375, #5457 ) ) REPRESENTATION_CONTEXT ( 'NONE', 'WORKASPACE' ) );
#3588=DIRECTION ( 'NONE',  ( 0.000000000000000000, 0.000000000000000000, -1.000000000000000000 ) ) ;
#3595=DIRECTION ( 'NONE',  ( 1.000000000000000000, -0.000000000000000000, -0.000000000000000000 ) ) ;
#3596=ORIENTED_EDGE ( 'NONE', *, *, #8557, .F. ) ;
#3603=FACE_BOUND ( 'NONE', #17109, .T. ) ;
#3617=AXIS2_PLACEMENT_3D ( 'NONE', #15129, #1767, #11710 ) ;
#3629=CARTESIAN_POINT ( 'NONE',  ( -90.00000000000000000, 8.239576745513314221E-16, 6.728125000000023448 ) ) ;
#3646=AXIS2_PLACEMENT_3D ( 'NONE', #5472, #169, #18628 ) ;
#3666=AXIS2_PLACEMENT_3D ( 'NONE', #9119, #15754, #21053 ) ;
#3678=CARTESIAN_POINT ( 'NONE',  ( 1.129531546211711479, 0.000000000000000000, 0.000000000000000000 ) ) ;
#3690=CARTESIAN_POINT ( 'NONE',  ( 1.400000000000000133, 0.000000000000000000, 0.000000000000000000 ) ) ;
#3703=ORIENTED_EDGE ( 'NONE', *, *, #14153, .T. ) ;
#3734=DIRECTION ( 'NONE',  ( 1.000000000000000000, 0.000000000000000000, 0.000000000000000000 ) ) ;
#3735=ADVANCED_FACE ( 'NONE', ( #2635 ), #7669, .T. ) ;
#3742=ORIENTED_EDGE ( 'NONE', *, *, #13016, .F. ) ;
#3761=ADVANCED_FACE ( 'NONE', ( #7296 ), #12788, .F. ) ;
#3803=AXIS2_PLACEMENT_3D ( 'NONE', #10874, #14185, #20930 ) ;
#3822=DIRECTION ( 'NONE',  ( 1.000000000000000000, 0.000000000000000000, 0.000000000000000000 ) ) ;
#3829=VERTEX_POINT ( 'NONE', #13122 ) ;
#3841=AXIS2_PLACEMENT_3D ( 'NONE', #7067, #18448, #11702 ) ;
#3848=ORIENTED_EDGE ( 'NONE', *, *, #7755, .F. ) ;
#3867=DIRECTION ( 'NONE',  ( 0.000000000000000000, 0.000000000000000000, -1.000000000000000000 ) ) ;
#3875=ORIENTED_EDGE ( 'NONE', *, *, #17699, .F. ) ;
#3885=CARTESIAN_POINT ( 'NONE',  ( 1.114299999999999846, 0.000000000000000000, 0.000000000000000000 ) ) ;
#3890=DIRECTION ( 'NONE',  ( 1.000000000000000000, 0.000000000000000000, 0.000000000000000000 ) ) ;
#3923=ORIENTED_EDGE ( 'NONE', *, *, #19982, .F. ) ;
#3928=EDGE_CURVE ( 'NONE', #16790, #17309, #18279, .T. ) ;
#3933=ORIENTED_EDGE ( 'NONE', *, *, #957, .F. ) ;
#3952=EDGE_CURVE ( 'NONE', #21211, #16727, #620, .T. ) ;
#3971=CARTESIAN_POINT ( 'NONE',  ( 1.129531546211678616, 0.000000000000000000, -6.887500000000022382 ) ) ;
#3975=AXIS2_PLACEMENT_3D ( 'NONE', #4210, #16137, #6204 ) ;
#4022=VERTEX_POINT ( 'NONE', #9327 ) ;
#4045=DIRECTION ( 'NONE',  ( -1.000000000000000000, 0.000000000000000000, 0.000000000000000000 ) ) ;
#4055=ORIENTED_EDGE ( 'NONE', *, *, #14466, .T. ) ;
#4070=DIRECTION ( 'NONE',  ( -0.8831157194574072999, 5.745494457773168027E-17, -0.4691552259617553511 ) ) ;
#4078=TOROIDAL_SURFACE ( 'NONE', #17142, 5.100000000000000533, 0.09999999999999971412 ) ;
#4122=ORIENTED_EDGE ( 'NONE', *, *, #12560, .T. ) ;
#4156=LINE ( 'NONE', #13988, #16373 ) ;
#4176=ORIENTED_EDGE ( 'NONE', *, *, #9350, .T. ) ;
#4180=CARTESIAN_POINT ( 'NONE',  ( -1.500000000000001332, 0.000000000000000000, -6.728125000000022560 ) ) ;
#4190=CARTESIAN_POINT ( 'NONE',  ( -1.129531546211723025, 6.886005254585696675E-16, 5.612499999999999822 ) ) ;
#4191=ADVANCED_FACE ( 'NONE', ( #6880 ), #1354, .T. ) ;
#4194=DIRECTION ( 'NONE',  ( 1.000000000000000000, 0.000000000000000000, 0.000000000000000000 ) ) ;
#4198=ORIENTED_EDGE ( 'NONE', *, *, #19627, .T. ) ;
#4210=CARTESIAN_POINT ( 'NONE',  ( -1.399999999999998579, 0.000000000000000000, 0.000000000000000000 ) ) ;
#4231=ORIENTED_EDGE ( 'NONE', *, *, #6542, .F. ) ;
#4235=ORIENTED_EDGE ( 'NONE', *, *, #9411, .F. ) ;
#4245=FACE_OUTER_BOUND ( 'NONE', #16699, .T. ) ;
#4246=DIRECTION ( 'NONE',  ( 0.000000000000000000, 0.000000000000000000, -1.000000000000000000 ) ) ;
#4254=DIRECTION ( 'NONE',  ( 1.000000000000000000, 0.000000000000000000, 0.000000000000000000 ) ) ;
#4262=DIRECTION ( 'NONE',  ( 1.000000000000000000, -0.000000000000000000, -0.000000000000000000 ) ) ;
#4297=EDGE_LOOP ( 'NONE', ( #2592, #3, #10888, #20448 ) ) ;
#4298=ADVANCED_BREP_SHAPE_REPRESENTATION ( '', ( #20897, #15567 ), #4640 ) ;
#4313=EDGE_CURVE ( 'NONE', #20799, #15070, #14380, .T. ) ;
#4336=DIRECTION ( 'NONE',  ( 1.000000000000000000, 0.000000000000000000, 0.000000000000000000 ) ) ;
#4359=EDGE_LOOP ( 'NONE', ( #12673, #7785, #8044, #18086 ) ) ;
#4360=AXIS2_PLACEMENT_3D ( 'NONE', #17090, #10338, #1952 ) ;
#4370=VECTOR ( 'NONE', #18075, 1000.000000000000000 ) ;
#4372=CARTESIAN_POINT ( 'NONE',  ( -1.500000000000001332, 0.000000000000000000, 0.000000000000000000 ) ) ;
#4375=CARTESIAN_POINT ( 'NONE',  ( 1.139999999999995239, 0.000000000000000000, 0.000000000000000000 ) ) ;
#4382=VERTEX_POINT ( 'NONE', #7630 ) ;
#4386=AXIS2_PLACEMENT_3D ( 'NONE', #9773, #8025, #11436 ) ;
#4407=CARTESIAN_POINT ( 'NONE',  ( -90.00000000000000000, 0.000000000000000000, 0.000000000000000000 ) ) ;
#4408=CARTESIAN_POINT ( 'NONE',  ( 1.499999999999999556, 7.400000000000020783, 0.000000000000000000 ) ) ;
#4429=FACE_OUTER_BOUND ( 'NONE', #8717, .T. ) ;
#4460=FACE_BOUND ( 'NONE', #3391, .T. ) ;
#4479=ORIENTED_EDGE ( 'NONE', *, *, #13496, .T. ) ;
#4493=EDGE_LOOP ( 'NONE', ( #9287, #18058, #16909, #16289 ) ) ;
#4496=CARTESIAN_POINT ( 'NONE',  ( -1.140000000000000124, 6.898680348956876061E-16, 5.633200000000004870 ) ) ;
#4506=DIRECTION ( 'NONE',  ( 1.000000000000000000, 0.000000000000000000, 0.000000000000000000 ) ) ;
#4519=ADVANCED_FACE ( 'NONE', ( #21547 ), #6530, .T. ) ;
#4570=CARTESIAN_POINT ( 'NONE',  ( -1.200000000000006617, 0.000000000000000000, 0.000000000000000000 ) ) ;
#4579=CIRCLE ( 'NONE', #14102, 6.728125000000022560 ) ;
#4583=( NAMED_UNIT ( * ) PLANE_ANGLE_UNIT ( ) SI_UNIT ( $, .RADIAN. ) );
#4593=ORIENTED_EDGE ( 'NONE', *, *, #6796, .T. ) ;
#4640=( GEOMETRIC_REPRESENTATION_CONTEXT ( 3 ) GLOBAL_UNCERTAINTY_ASSIGNED_CONTEXT ( ( #11670 ) ) GLOBAL_UNIT_ASSIGNED_CONTEXT ( ( #16722, #19933, #15724 ) ) REPRESENTATION_CONTEXT ( 'NONE', 'WORKASPACE' ) );
#4643=ADVANCED_FACE ( 'NONE', ( #6967, #15337 ), #5515, .T. ) ;
#4647=DIRECTION ( 'NONE',  ( 1.000000000000000000, 0.000000000000000000, 0.000000000000000000 ) ) ;
#4649=DIRECTION ( 'NONE',  ( -1.000000000000000000, 0.000000000000000000, -0.000000000000000000 ) ) ;
#4736=EDGE_CURVE ( 'NONE', #769, #2562, #18886, .T. ) ;
#4738=DIRECTION ( 'NONE',  ( 0.000000000000000000, 0.000000000000000000, -1.000000000000000000 ) ) ;
#4751=CARTESIAN_POINT ( 'NONE',  ( -90.00000000000000000, 0.000000000000000000, -7.500000000000020428 ) ) ;
#4765=EDGE_CURVE ( 'NONE', #6321, #1054, #11615, .T. ) ;
#4767=ORIENTED_EDGE ( 'NONE', *, *, #16665, .F. ) ;
#4809=CARTESIAN_POINT ( 'NONE',  ( -90.00000000000000000, 0.000000000000000000, -6.887500000000022382 ) ) ;
#4825=ORIENTED_EDGE ( 'NONE', *, *, #712, .T. ) ;
#4840=CARTESIAN_POINT ( 'NONE',  ( -90.00000000000000000, 8.434754829127421589E-16, 6.887500000000022382 ) ) ;
#4841=CARTESIAN_POINT ( 'NONE',  ( -1.139999999999998570, 0.000000000000000000, 0.000000000000000000 ) ) ;
#4857=ORIENTED_EDGE ( 'NONE', *, *, #13644, .T. ) ;
#4866=EDGE_CURVE ( 'NONE', #3210, #5078, #14065, .T. ) ;
#4896=FACE_OUTER_BOUND ( 'NONE', #4493, .T. ) ;
#4912=VERTEX_POINT ( 'NONE', #4180 ) ;
#4922=CARTESIAN_POINT ( 'NONE',  ( 1.500000000000000888, 6.245698675651501825E-16, 5.100000000000000533 ) ) ;
#4958=DIRECTION ( 'NONE',  ( 1.000000000000000000, 0.000000000000000000, 0.000000000000000000 ) ) ;
#4976=AXIS2_PLACEMENT_3D ( 'NONE', #13004, #4506, #3062 ) ;
#4987=CARTESIAN_POINT ( 'NONE',  ( 1.500000000000001332, 0.000000000000000000, 5.453125000000000000 ) ) ;
#5025=AXIS2_PLACEMENT_3D ( 'NONE', #2033, #13634, #20386 ) ;
#5078=VERTEX_POINT ( 'NONE', #10130 ) ;
#5107=ORIENTED_EDGE ( 'NONE', *, *, #6656, .F. ) ;
#5141=TOROIDAL_SURFACE ( 'NONE', #17495, 5.633200000000004870, 0.02569999999999482421 ) ;
#5153=DIRECTION ( 'NONE',  ( 1.000000000000000000, 0.000000000000000000, 0.000000000000000000 ) ) ;
#5169=ORIENTED_EDGE ( 'NONE', *, *, #20300, .F. ) ;
#5189=ORIENTED_EDGE ( 'NONE', *, *, #17441, .T. ) ;
#5214=TOROIDAL_SURFACE ( 'NONE', #18624, 6.866799999999992465, 0.02569999999999482421 ) ;
#5257=CIRCLE ( 'NONE', #9830, 5.633200000000004870 ) ;
#5283=FACE_OUTER_BOUND ( 'NONE', #19497, .T. ) ;
#5321=EDGE_CURVE ( 'NONE', #20994, #13440, #1043, .T. ) ;
#5337=CARTESIAN_POINT ( 'NONE',  ( 1.114299999999999846, 0.000000000000000000, -6.866799999999992465 ) ) ;
#5354=DIRECTION ( 'NONE',  ( 0.000000000000000000, 0.000000000000000000, -1.000000000000000000 ) ) ;
#5368=LINE ( 'NONE', #5693, #20794 ) ;
#5391=DIRECTION ( 'NONE',  ( 0.000000000000000000, 0.000000000000000000, -1.000000000000000000 ) ) ;
#5392=EDGE_CURVE ( 'NONE', #4912, #826, #4579, .T. ) ;
#5394=DIRECTION ( 'NONE',  ( 1.000000000000000000, 0.000000000000000000, 0.000000000000000000 ) ) ;
#5401=CIRCLE ( 'NONE', #3975, 7.500000000000020428 ) ;
#5410=AXIS2_PLACEMENT_3D ( 'NONE', #11656, #8550, #18402 ) ;
#5441=CIRCLE ( 'NONE', #3666, 5.453125000000000000 ) ;
#5457=( NAMED_UNIT ( * ) SI_UNIT ( $, .STERADIAN. ) SOLID_ANGLE_UNIT ( ) );
#5472=CARTESIAN_POINT ( 'NONE',  ( -90.00000000000000000, 0.000000000000000000, 0.000000000000000000 ) ) ;
#5476=VECTOR ( 'NONE', #9243, 1000.000000000000000 ) ;
#5514=AXIS2_PLACEMENT_3D ( 'NONE', #3073, #13339, #13448 ) ;
#5515=PLANE ( 'NONE',  #19714 ) ;
#5518=CARTESIAN_POINT ( 'NONE',  ( -1.114300000000000290, 0.000000000000000000, -6.866799999999992465 ) ) ;
#5525=VECTOR ( 'NONE', #13026, 1000.000000000000000 ) ;
#5536=ORIENTED_EDGE ( 'NONE', *, *, #7209, .F. ) ;
#5554=CIRCLE ( 'NONE', #13324, 5.612499999999999822 ) ;
#5555=CIRCLE ( 'NONE', #14736, 0.1000000000000002554 ) ;
#5567=DIRECTION ( 'NONE',  ( 1.000000000000000000, 0.000000000000000000, 0.000000000000000000 ) ) ;
#5598=ORIENTED_EDGE ( 'NONE', *, *, #14466, .F. ) ;
#5630=DIRECTION ( 'NONE',  ( -0.000000000000000000, 0.000000000000000000, 1.000000000000000000 ) ) ;
#5693=CARTESIAN_POINT ( 'NONE',  ( -90.00000000000000000, 0.000000000000000000, -6.728125000000023448 ) ) ;
#5718=CIRCLE ( 'NONE', #2888, 6.866799999999992465 ) ;
#5721=PLANE ( 'NONE',  #8436 ) ;
#5730=EDGE_CURVE ( 'NONE', #3829, #1128, #5401, .T. ) ;
#5739=AXIS2_PLACEMENT_3D ( 'NONE', #9592, #6203, #12922 ) ;
#5750=ORIENTED_EDGE ( 'NONE', *, *, #6253, .T. ) ;
#5800=ORIENTED_EDGE ( 'NONE', *, *, #19314, .T. ) ;
#5808=AXIS2_PLACEMENT_3D ( 'NONE', #15677, #17130, #656 ) ;
#5825=VECTOR ( 'NONE', #4070, 1000.000000000000114 ) ;
#5832=CIRCLE ( 'NONE', #18186, 0.02570000000000176310 ) ;
#5840=ORIENTED_EDGE ( 'NONE', *, *, #8557, .T. ) ;
#5850=CIRCLE ( 'NONE', #6550, 5.612499999999999822 ) ;
#5861=CARTESIAN_POINT ( 'NONE',  ( -90.00000000000000000, 0.000000000000000000, -6.728125000000022560 ) ) ;
#5958=VECTOR ( 'NONE', #17659, 1000.000000000000000 ) ;
#6024=EDGE_CURVE ( 'NONE', #20241, #6321, #6815, .T. ) ;
#6029=ORIENTED_EDGE ( 'NONE', *, *, #18283, .F. ) ;
#6047=DIRECTION ( 'NONE',  ( 1.000000000000000000, 0.000000000000000000, 0.000000000000000000 ) ) ;
#6058=ORIENTED_EDGE ( 'NONE', *, *, #14307, .T. ) ;
#6067=LINE ( 'NONE', #19206, #5825 ) ;
#6138=SURFACE_STYLE_FILL_AREA ( #930 ) ;
#6139=ADVANCED_FACE ( 'NONE', ( #7499 ), #9474, .T. ) ;
#6151=AXIS2_PLACEMENT_3D ( 'NONE', #11226, #6047, #9225 ) ;
#6159=ORIENTED_EDGE ( 'NONE', *, *, #5730, .F. ) ;
#6174=CARTESIAN_POINT ( 'NONE',  ( 1.139999999999998570, 0.000000000000000000, 0.000000000000000000 ) ) ;
#6180=DIRECTION ( 'NONE',  ( 0.000000000000000000, 0.000000000000000000, -1.000000000000000000 ) ) ;
#6183=AXIS2_PLACEMENT_3D ( 'NONE', #16891, #17104, #1855 ) ;
#6186=DIRECTION ( 'NONE',  ( 1.000000000000000000, 0.000000000000000000, 0.000000000000000000 ) ) ;
#6203=DIRECTION ( 'NONE',  ( 1.000000000000000000, 0.000000000000000000, 0.000000000000000000 ) ) ;
#6204=DIRECTION ( 'NONE',  ( 0.000000000000000000, 0.000000000000000000, -1.000000000000000000 ) ) ;
#6242=CARTESIAN_POINT ( 'NONE',  ( -1.139999999999999680, 6.866799999999992465, 0.000000000000000000 ) ) ;
#6253=EDGE_CURVE ( 'NONE', #3210, #20994, #1530, .T. ) ;
#6257=EDGE_LOOP ( 'NONE', ( #7313, #3031 ) ) ;
#6262=VERTEX_POINT ( 'NONE', #16659 ) ;
#6273=EDGE_CURVE ( 'NONE', #5078, #13440, #17416, .T. ) ;
#6274=EDGE_LOOP ( 'NONE', ( #19688, #11925, #4231, #18489 ) ) ;
#6295=DIRECTION ( 'NONE',  ( 0.000000000000000000, 0.000000000000000000, -1.000000000000000000 ) ) ;
#6321=VERTEX_POINT ( 'NONE', #18755 ) ;
#6335=ORIENTED_EDGE ( 'NONE', *, *, #11225, .T. ) ;
#6357=PLANE ( 'NONE',  #6507 ) ;
#6398=VERTEX_POINT ( 'NONE', #8810 ) ;
#6409=CYLINDRICAL_SURFACE ( 'NONE', #8540, 6.887500000000022382 ) ;
#6410=DIRECTION ( 'NONE',  ( 0.000000000000000000, 0.000000000000000000, -1.000000000000000000 ) ) ;
#6436=EDGE_LOOP ( 'NONE', ( #8519, #16616, #6159, #13847 ) ) ;
#6457=DIRECTION ( 'NONE',  ( 0.000000000000000000, 0.000000000000000000, 1.000000000000000000 ) ) ;
#6469=CIRCLE ( 'NONE', #3291, 6.887500000000022382 ) ;
#6473=CARTESIAN_POINT ( 'NONE',  ( -90.00000000000000000, 0.000000000000000000, -5.000000000000000888 ) ) ;
#6507=AXIS2_PLACEMENT_3D ( 'NONE', #6242, #1368, #6457 ) ;
#6509=CARTESIAN_POINT ( 'NONE',  ( -1.500000000000001332, 8.239576745513313235E-16, 6.728125000000022560 ) ) ;
#6518=DIRECTION ( 'NONE',  ( 0.000000000000000000, 0.000000000000000000, -1.000000000000000000 ) ) ;
#6530=CYLINDRICAL_SURFACE ( 'NONE', #21469, 5.612499999999999822 ) ;
#6542=EDGE_CURVE ( 'NONE', #17273, #6557, #14946, .T. ) ;
#6550=AXIS2_PLACEMENT_3D ( 'NONE', #13431, #1407, #1294 ) ;
#6557=VERTEX_POINT ( 'NONE', #21062 ) ;
#6632=FACE_OUTER_BOUND ( 'NONE', #932, .T. ) ;
#6656=EDGE_CURVE ( 'NONE', #826, #1308, #8347, .T. ) ;
#6657=VERTEX_POINT ( 'NONE', #13312 ) ;
#6671=ORIENTED_EDGE ( 'NONE', *, *, #21697, .T. ) ;
#6682=CIRCLE ( 'NONE', #1013, 5.633200000000004870 ) ;
#6699=EDGE_CURVE ( 'NONE', #12588, #21211, #15674, .T. ) ;
#6714=CARTESIAN_POINT ( 'NONE',  ( -90.00000000000000000, 0.000000000000000000, 0.000000000000000000 ) ) ;
#6738=CARTESIAN_POINT ( 'NONE',  ( 1.500000000000001332, 0.000000000000000000, 0.000000000000000000 ) ) ;
#6777=VERTEX_POINT ( 'NONE', #3483 ) ;
#6790=CARTESIAN_POINT ( 'NONE',  ( 1.139999999999998570, 0.000000000000000000, -6.866799999999992465 ) ) ;
#6796=EDGE_CURVE ( 'NONE', #14440, #13819, #17069, .T. ) ;
#6811=ADVANCED_FACE ( 'NONE', ( #18734 ), #7023, .T. ) ;
#6815=CIRCLE ( 'NONE', #19509, 0.02570000000000176310 ) ;
#6880=FACE_OUTER_BOUND ( 'NONE', #17996, .T. ) ;
#6906=ORIENTED_EDGE ( 'NONE', *, *, #18781, .T. ) ;
#6949=CIRCLE ( 'NONE', #19980, 0.02569999999999482421 ) ;
#6967=FACE_BOUND ( 'NONE', #14250, .T. ) ;
#6996=DIRECTION ( 'NONE',  ( 0.000000000000000000, 0.000000000000000000, -1.000000000000000000 ) ) ;
#7007=ORIENTED_EDGE ( 'NONE', *, *, #4736, .T. ) ;
#7023=CYLINDRICAL_SURFACE ( 'NONE', #13905, 7.500000000000020428 ) ;
#7028=DIRECTION ( 'NONE',  ( 0.000000000000000000, 0.000000000000000000, -1.000000000000000000 ) ) ;
#7037=CARTESIAN_POINT ( 'NONE',  ( 1.129531546211678616, 8.434754829127421589E-16, 6.887500000000022382 ) ) ;
#7067=CARTESIAN_POINT ( 'NONE',  ( 1.114299999999999846, 8.409404640385035208E-16, 6.866799999999992465 ) ) ;
#7086=DIRECTION ( 'NONE',  ( 1.000000000000000000, -0.000000000000000000, -0.000000000000000000 ) ) ;
#7106=DIRECTION ( 'NONE',  ( 0.000000000000000000, 0.000000000000000000, -1.000000000000000000 ) ) ;
#7178=DIRECTION ( 'NONE',  ( 0.000000000000000000, 0.000000000000000000, -1.000000000000000000 ) ) ;
#7197=DIRECTION ( 'NONE',  ( 1.000000000000000000, -0.000000000000000000, -0.000000000000000000 ) ) ;
#7201=DIRECTION ( 'NONE',  ( 1.000000000000000000, 0.000000000000000000, 0.000000000000000000 ) ) ;
#7209=EDGE_CURVE ( 'NONE', #12422, #1308, #16746, .T. ) ;
#7249=CYLINDRICAL_SURFACE ( 'NONE', #9852, 5.000000000000000888 ) ;
#7274=CARTESIAN_POINT ( 'NONE',  ( 1.199999999999992628, 0.000000000000000000, 0.000000000000000000 ) ) ;
#7283=AXIS2_PLACEMENT_3D ( 'NONE', #1556, #3105, #16923 ) ;
#7296=FACE_OUTER_BOUND ( 'NONE', #11098, .T. ) ;
#7298=AXIS2_PLACEMENT_3D ( 'NONE', #15217, #2967, #18230 ) ;
#7313=ORIENTED_EDGE ( 'NONE', *, *, #14205, .F. ) ;
#7371=DIRECTION ( 'NONE',  ( 1.000000000000000000, 0.000000000000000000, 0.000000000000000000 ) ) ;
#7375=DIRECTION ( 'NONE',  ( 1.000000000000000000, -0.000000000000000000, -0.000000000000000000 ) ) ;
#7388=EDGE_LOOP ( 'NONE', ( #18469, #606 ) ) ;
#7396=ORIENTED_EDGE ( 'NONE', *, *, #6656, .T. ) ;
#7401=DIRECTION ( 'NONE',  ( 0.000000000000000000, 0.000000000000000000, -1.000000000000000000 ) ) ;
#7406=AXIS2_PLACEMENT_3D ( 'NONE', #21149, #18157, #2682 ) ;
#7414=EDGE_LOOP ( 'NONE', ( #14475, #6335, #16176, #14312 ) ) ;
#7424=DIRECTION ( 'NONE',  ( 1.000000000000000000, 0.000000000000000000, 0.000000000000000000 ) ) ;
#7439=DIRECTION ( 'NONE',  ( 0.000000000000000000, 0.000000000000000000, -1.000000000000000000 ) ) ;
#7459=CARTESIAN_POINT ( 'NONE',  ( -1.129531546211723025, 0.000000000000000000, 0.000000000000000000 ) ) ;
#7462=DIRECTION ( 'NONE',  ( 1.000000000000000000, 0.000000000000000000, 0.000000000000000000 ) ) ;
#7489=DIRECTION ( 'NONE',  ( 0.000000000000000000, 0.000000000000000000, 1.000000000000000000 ) ) ;
#7498=DIRECTION ( 'NONE',  ( 0.000000000000000000, 0.000000000000000000, 1.000000000000000000 ) ) ;
#7499=FACE_OUTER_BOUND ( 'NONE', #4359, .T. ) ;
#7543=CARTESIAN_POINT ( 'NONE',  ( 1.500000000000001332, 0.000000000000000000, 0.000000000000000000 ) ) ;
#7607=CARTESIAN_POINT ( 'NONE',  ( -1.399999999999999911, 6.245698675651501825E-16, 5.100000000000000533 ) ) ;
#7630=CARTESIAN_POINT ( 'NONE',  ( 1.200000000000006617, 6.873330160214519262E-16, 5.612499999999999822 ) ) ;
#7631=ORIENTED_EDGE ( 'NONE', *, *, #18765, .T. ) ;
#7669=TOROIDAL_SURFACE ( 'NONE', #9415, 6.866799999999992465, 0.02569999999999482421 ) ;
#7675=SURFACE_SIDE_STYLE ('',( #6138 ) ) ;
#7714=ORIENTED_EDGE ( 'NONE', *, *, #19627, .F. ) ;
#7735=AXIS2_PLACEMENT_3D ( 'NONE', #18323, #1621, #20296 ) ;
#7737=AXIS2_PLACEMENT_3D ( 'NONE', #2508, #8820, #15557 ) ;
#7741=EDGE_LOOP ( 'NONE', ( #19913, #7396, #15805, #21083 ) ) ;
#7746=PLANE ( 'NONE',  #5514 ) ;
#7755=EDGE_CURVE ( 'NONE', #15070, #20799, #2230, .T. ) ;
#7767=VERTEX_POINT ( 'NONE', #4922 ) ;
#7780=CARTESIAN_POINT ( 'NONE',  ( 1.114299999999999846, 6.898680348956876061E-16, 5.633200000000004870 ) ) ;
#7785=ORIENTED_EDGE ( 'NONE', *, *, #9726, .T. ) ;
#7801=DIRECTION ( 'NONE',  ( 0.000000000000000000, 1.224646799147324364E-16, 1.000000000000000000 ) ) ;
#7804=ADVANCED_FACE ( 'NONE', ( #1591 ), #8338, .F. ) ;
#7805=EDGE_LOOP ( 'NONE', ( #6029, #16972, #21019, #3923 ) ) ;
#7821=CARTESIAN_POINT ( 'NONE',  ( 1.500000000000001332, 0.000000000000000000, 5.453125000000000000 ) ) ;
#7888=EDGE_CURVE ( 'NONE', #21408, #11959, #18816, .T. ) ;
#7899=EDGE_LOOP ( 'NONE', ( #3703, #6906, #39, #17953 ) ) ;
#7925=DIRECTION ( 'NONE',  ( -0.000000000000000000, 0.000000000000000000, 1.000000000000000000 ) ) ;
#7954=AXIS2_PLACEMENT_3D ( 'NONE', #3678, #3575, #10205 ) ;
#8002=DIRECTION ( 'NONE',  ( 0.000000000000000000, 0.000000000000000000, -1.000000000000000000 ) ) ;
#8006=AXIS2_PLACEMENT_3D ( 'NONE', #8595, #5394, #12234 ) ;
#8015=ORIENTED_EDGE ( 'NONE', *, *, #19752, .T. ) ;
#8025=DIRECTION ( 'NONE',  ( -0.000000000000000000, -1.000000000000000000, -0.000000000000000000 ) ) ;
#8032=CARTESIAN_POINT ( 'NONE',  ( 1.200000000000006617, 0.000000000000000000, -5.612499999999999822 ) ) ;
#8041=TOROIDAL_SURFACE ( 'NONE', #20391, 7.400000000000019895, 0.1000000000000006994 ) ;
#8044=ORIENTED_EDGE ( 'NONE', *, *, #15811, .F. ) ;
#8045=CARTESIAN_POINT ( 'NONE',  ( -1.500000000000000666, 6.728125000000022560, 0.000000000000000000 ) ) ;
#8046=ORIENTED_EDGE ( 'NONE', *, *, #6024, .F. ) ;
#8051=CARTESIAN_POINT ( 'NONE',  ( 1.500000000000001332, 0.000000000000000000, -6.728125000000023448 ) ) ;
#8072=DIRECTION ( 'NONE',  ( 1.000000000000000000, 0.000000000000000000, 0.000000000000000000 ) ) ;
#8084=TOROIDAL_SURFACE ( 'NONE', #7737, 5.100000000000000533, 0.1000000000000000472 ) ;
#8099=DIRECTION ( 'NONE',  ( 0.000000000000000000, 0.000000000000000000, -1.000000000000000000 ) ) ;
#8120=CARTESIAN_POINT ( 'NONE',  ( -1.399999999999998579, 0.000000000000000000, -5.000000000000000888 ) ) ;
#8166=CARTESIAN_POINT ( 'NONE',  ( -1.500000000000001332, 0.000000000000000000, -5.453125000000000000 ) ) ;
#8169=ADVANCED_FACE ( 'NONE', ( #14608 ), #822, .T. ) ;
#8171=FACE_OUTER_BOUND ( 'NONE', #11118, .T. ) ;
#8228=DIRECTION ( 'NONE',  ( 0.000000000000000000, -1.000000000000000000, 0.000000000000000000 ) ) ;
#8249=CARTESIAN_POINT ( 'NONE',  ( -1.200000000000006617, 0.000000000000000000, -5.612499999999999822 ) ) ;
#8254=ADVANCED_FACE ( 'NONE', ( #18749, #3603 ), #16873, .T. ) ;
#8264=DIRECTION ( 'NONE',  ( 0.000000000000000000, 0.000000000000000000, -1.000000000000000000 ) ) ;
#8266=CARTESIAN_POINT ( 'NONE',  ( -1.500000000000001332, 0.000000000000000000, 0.000000000000000000 ) ) ;
#8267=AXIS2_PLACEMENT_3D ( 'NONE', #1482, #8228, #13521 ) ;
#8295=LINE ( 'NONE', #2776, #18252 ) ;
#8304=CIRCLE ( 'NONE', #19958, 5.612499999999999822 ) ;
#8331=EDGE_LOOP ( 'NONE', ( #3875, #7007, #10100, #12049 ) ) ;
#8338=CYLINDRICAL_SURFACE ( 'NONE', #5410, 5.000000000000000888 ) ;
#8342=EDGE_LOOP ( 'NONE', ( #8015, #4479, #4767, #17581 ) ) ;
#8347=LINE ( 'NONE', #19947, #4370 ) ;
#8357=ORIENTED_EDGE ( 'NONE', *, *, #13767, .F. ) ;
#8369=AXIS2_PLACEMENT_3D ( 'NONE', #12578, #15571, #7178 ) ;
#8413=EDGE_CURVE ( 'NONE', #8785, #13868, #5441, .T. ) ;
#8436=AXIS2_PLACEMENT_3D ( 'NONE', #745, #12127, #530 ) ;
#8458=ORIENTED_EDGE ( 'NONE', *, *, #9984, .T. ) ;
#8491=EDGE_CURVE ( 'NONE', #15070, #21459, #2706, .T. ) ;
#8511=DIRECTION ( 'NONE',  ( 1.000000000000000000, 0.000000000000000000, 0.000000000000000000 ) ) ;
#8519=ORIENTED_EDGE ( 'NONE', *, *, #16501, .T. ) ;
#8533=DIRECTION ( 'NONE',  ( 0.000000000000000000, 0.000000000000000000, -1.000000000000000000 ) ) ;
#8538=DIRECTION ( 'NONE',  ( 1.000000000000000000, 0.000000000000000000, 0.000000000000000000 ) ) ;
#8540=AXIS2_PLACEMENT_3D ( 'NONE', #14891, #21627, #8264 ) ;
#8550=DIRECTION ( 'NONE',  ( 1.000000000000000000, 0.000000000000000000, 0.000000000000000000 ) ) ;
#8557=EDGE_CURVE ( 'NONE', #20994, #17054, #11429, .T. ) ;
#8576=EDGE_CURVE ( 'NONE', #10685, #17273, #17787, .T. ) ;
#8595=CARTESIAN_POINT ( 'NONE',  ( 1.199999999999992628, 0.000000000000000000, 0.000000000000000000 ) ) ;
#8600=DIRECTION ( 'NONE',  ( 1.000000000000000000, -0.000000000000000000, -0.000000000000000000 ) ) ;
#8605=ORIENTED_EDGE ( 'NONE', *, *, #3952, .T. ) ;
#8632=VECTOR ( 'NONE', #13117, 1000.000000000000114 ) ;
#8645=ADVANCED_FACE ( 'NONE', ( #21815 ), #499, .T. ) ;
#8647=EDGE_CURVE ( 'NONE', #13868, #8785, #21313, .T. ) ;
#8658=ORIENTED_EDGE ( 'NONE', *, *, #8413, .F. ) ;
#8703=CIRCLE ( 'NONE', #928, 6.887500000000022382 ) ;
#8717=EDGE_LOOP ( 'NONE', ( #16644, #8658 ) ) ;
#8734=EDGE_LOOP ( 'NONE', ( #19798, #18935, #17815, #14604 ) ) ;
#8777=EDGE_CURVE ( 'NONE', #9461, #2562, #12855, .T. ) ;
#8785=VERTEX_POINT ( 'NONE', #20911 ) ;
#8801=ORIENTED_EDGE ( 'NONE', *, *, #20622, .F. ) ;
#8810=CARTESIAN_POINT ( 'NONE',  ( 1.139999999999995017, 6.898680348956876061E-16, 5.633200000000004870 ) ) ;
#8820=DIRECTION ( 'NONE',  ( 1.000000000000000000, 0.000000000000000000, 0.000000000000000000 ) ) ;
#8834=CARTESIAN_POINT ( 'NONE',  ( 1.199999999999992628, 0.000000000000000000, 0.000000000000000000 ) ) ;
#8859=CARTESIAN_POINT ( 'NONE',  ( 1.129531546211711479, 6.886005254585696675E-16, 5.612499999999999822 ) ) ;
#8863=ORIENTED_EDGE ( 'NONE', *, *, #16482, .F. ) ;
#8904=EDGE_CURVE ( 'NONE', #18616, #14552, #1570, .T. ) ;
#8920=ORIENTED_EDGE ( 'NONE', *, *, #2281, .F. ) ;
#8986=TOROIDAL_SURFACE ( 'NONE', #16033, 5.100000000000000533, 0.1000000000000000472 ) ;
#8989=DIRECTION ( 'NONE',  ( 1.000000000000000000, -0.000000000000000000, -0.000000000000000000 ) ) ;
#9009=AXIS2_PLACEMENT_3D ( 'NONE', #18184, #1162, #11759 ) ;
#9026=ORIENTED_EDGE ( 'NONE', *, *, #2391, .T. ) ;
#9036=LINE ( 'NONE', #2301, #5476 ) ;
#9064=CIRCLE ( 'NONE', #13665, 6.887500000000022382 ) ;
#9086=( LENGTH_UNIT ( ) NAMED_UNIT ( * ) SI_UNIT ( .MILLI., .METRE. ) );
#9091=DIRECTION ( 'NONE',  ( 0.000000000000000000, 0.000000000000000000, -1.000000000000000000 ) ) ;
#9111=CIRCLE ( 'NONE', #19014, 0.1000000000000002554 ) ;
#9119=CARTESIAN_POINT ( 'NONE',  ( -1.500000000000001332, 0.000000000000000000, 0.000000000000000000 ) ) ;
#9123=CARTESIAN_POINT ( 'NONE',  ( -1.399999999999998579, 9.184850993605175555E-16, 7.500000000000020428 ) ) ;
#9136=CARTESIAN_POINT ( 'NONE',  ( 1.500000000000001332, 0.000000000000000000, 0.000000000000000000 ) ) ;
#9156=STYLED_ITEM ( 'NONE', ( #21163 ), #20897 ) ;
#9170=DIRECTION ( 'NONE',  ( 0.000000000000000000, 0.000000000000000000, -1.000000000000000000 ) ) ;
#9180=AXIS2_PLACEMENT_3D ( 'NONE', #8045, #19641, #7925 ) ;
#9205=EDGE_CURVE ( 'NONE', #11959, #16727, #6067, .T. ) ;
#9225=DIRECTION ( 'NONE',  ( 0.000000000000000000, 0.000000000000000000, -1.000000000000000000 ) ) ;
#9230=EDGE_CURVE ( 'NONE', #20799, #19543, #9036, .T. ) ;
#9243=DIRECTION ( 'NONE',  ( 1.000000000000000000, 0.000000000000000000, 0.000000000000000000 ) ) ;
#9245=DIRECTION ( 'NONE',  ( 1.000000000000000000, 0.000000000000000000, 0.000000000000000000 ) ) ;
#9257=PRODUCT_DEFINITION ( 'UNKNOWN', '', #20527, #17126 ) ;
#9287=ORIENTED_EDGE ( 'NONE', *, *, #18292, .F. ) ;
#9315=DIRECTION ( 'NONE',  ( 0.8831157194574072999, 5.745494457773168027E-17, 0.4691552259617553511 ) ) ;
#9327=CARTESIAN_POINT ( 'NONE',  ( -1.500000000000001332, 9.123618653647806797E-16, 7.400000000000019895 ) ) ;
#9333=DIRECTION ( 'NONE',  ( 0.000000000000000000, 1.000000000000000000, -1.224646799147353207E-16 ) ) ;
#9350=EDGE_CURVE ( 'NONE', #20994, #3210, #10395, .T. ) ;
#9365=EDGE_CURVE ( 'NONE', #21408, #4382, #1515, .T. ) ;
#9368=DIRECTION ( 'NONE',  ( 0.000000000000000000, 0.000000000000000000, -1.000000000000000000 ) ) ;
#9402=ORIENTED_EDGE ( 'NONE', *, *, #7888, .T. ) ;
#9405=DIRECTION ( 'NONE',  ( 0.000000000000000000, 0.000000000000000000, -1.000000000000000000 ) ) ;
#9411=EDGE_CURVE ( 'NONE', #14552, #1054, #21735, .T. ) ;
#9412=FACE_OUTER_BOUND ( 'NONE', #21826, .T. ) ;
#9415=AXIS2_PLACEMENT_3D ( 'NONE', #19326, #14132, #9368 ) ;
#9431=ORIENTED_EDGE ( 'NONE', *, *, #4866, .F. ) ;
#9450=ORIENTED_EDGE ( 'NONE', *, *, #16482, .T. ) ;
#9461=VERTEX_POINT ( 'NONE', #8051 ) ;
#9474=CYLINDRICAL_SURFACE ( 'NONE', #2233, 7.500000000000020428 ) ;
#9550=DIRECTION ( 'NONE',  ( 0.000000000000000000, 0.000000000000000000, -1.000000000000000000 ) ) ;
#9590=CIRCLE ( 'NONE', #5739, 5.000000000000000000 ) ;
#9592=CARTESIAN_POINT ( 'NONE',  ( 1.399999999999998579, 0.000000000000000000, 0.000000000000000000 ) ) ;
#9597=PLANE ( 'NONE',  #15409 ) ;
#9623=AXIS2_PLACEMENT_3D ( 'NONE', #3484, #13757, #2148 ) ;
#9642=PRODUCT ( 'instrument roller bearing_iso_ISO 1224 - 171015 - R,24,SI,NC,24', 'instrument roller bearing_iso_ISO 1224 - 171015 - R,24,SI,NC,24', '', ( #12832 ) ) ;
#9683=DIRECTION ( 'NONE',  ( 1.000000000000000000, 0.000000000000000000, 0.000000000000000000 ) ) ;
#9704=ORIENTED_EDGE ( 'NONE', *, *, #14050, .T. ) ;
#9705=CARTESIAN_POINT ( 'NONE',  ( -90.00000000000000000, 6.123233995736767268E-16, 5.000000000000000888 ) ) ;
#9726=EDGE_CURVE ( 'NONE', #1128, #18258, #4156, .T. ) ;
#9735=CIRCLE ( 'NONE', #7283, 7.400000000000020783 ) ;
#9751=CIRCLE ( 'NONE', #8006, 6.728125000000023448 ) ;
#9763=ORIENTED_EDGE ( 'NONE', *, *, #20431, .F. ) ;
#9773=CARTESIAN_POINT ( 'NONE',  ( 1.114299999999999846, 0.000000000000000000, -5.633200000000004870 ) ) ;
#9830=AXIS2_PLACEMENT_3D ( 'NONE', #4375, #16199, #9550 ) ;
#9837=PRODUCT_DEFINITION_SHAPE ( 'NONE', 'NONE',  #9257 ) ;
#9852=AXIS2_PLACEMENT_3D ( 'NONE', #1945, #3822, #397 ) ;
#9883=ORIENTED_EDGE ( 'NONE', *, *, #6273, .F. ) ;
#9896=CARTESIAN_POINT ( 'NONE',  ( 1.399999999999998579, 0.000000000000000000, 0.000000000000000000 ) ) ;
#9984=EDGE_CURVE ( 'NONE', #17955, #14440, #14625, .T. ) ;
#9997=CIRCLE ( 'NONE', #9623, 7.500000000000020428 ) ;
#10021=FACE_OUTER_BOUND ( 'NONE', #6436, .T. ) ;
#10033=ADVANCED_FACE ( 'NONE', ( #18836 ), #8986, .T. ) ;
#10044=AXIS2_PLACEMENT_3D ( 'NONE', #12347, #2178, #15216 ) ;
#10095=ORIENTED_EDGE ( 'NONE', *, *, #8491, .F. ) ;
#10100=ORIENTED_EDGE ( 'NONE', *, *, #17539, .T. ) ;
#10130=CARTESIAN_POINT ( 'NONE',  ( -1.500000000000000444, 6.245698675651501825E-16, 5.100000000000000533 ) ) ;
#10143=CARTESIAN_POINT ( 'NONE',  ( 1.400000000000000133, 0.000000000000000000, -5.100000000000000533 ) ) ;
#10197=CARTESIAN_POINT ( 'NONE',  ( -1.500000000000001332, 0.000000000000000000, 0.000000000000000000 ) ) ;
#10205=DIRECTION ( 'NONE',  ( 0.000000000000000000, 0.000000000000000000, 1.000000000000000000 ) ) ;
#10240=CARTESIAN_POINT ( 'NONE',  ( 1.399999999999999245, 0.000000000000000000, 0.000000000000000000 ) ) ;
#10251=FACE_OUTER_BOUND ( 'NONE', #8734, .T. ) ;
#10278=CARTESIAN_POINT ( 'NONE',  ( 1.500000000000001332, 0.000000000000000000, -7.400000000000020783 ) ) ;
#10320=CYLINDRICAL_SURFACE ( 'NONE', #3646, 6.887500000000022382 ) ;
#10338=DIRECTION ( 'NONE',  ( 1.000000000000000000, 0.000000000000000000, 0.000000000000000000 ) ) ;
#10346=CARTESIAN_POINT ( 'NONE',  ( -1.129531546211690385, 0.000000000000000000, 0.000000000000000000 ) ) ;
#10365=SHAPE_REPRESENTATION ( 'instrument roller bearing_iso_ISO 1224 - 171015 - R,24,SI,NC,24', ( #15567 ), #4640 ) ;
#10373=DIRECTION ( 'NONE',  ( 0.000000000000000000, 0.000000000000000000, -1.000000000000000000 ) ) ;
#10389=AXIS2_PLACEMENT_3D ( 'NONE', #20577, #3890, #20369 ) ;
#10395=CIRCLE ( 'NONE', #21348, 5.000000000000000888 ) ;
#10400=DIRECTION ( 'NONE',  ( -0.000000000000000000, -1.000000000000000000, -0.000000000000000000 ) ) ;
#10416=SURFACE_SIDE_STYLE ('',( #12297 ) ) ;
#10496=ORIENTED_EDGE ( 'NONE', *, *, #9205, .F. ) ;
#10512=FACE_OUTER_BOUND ( 'NONE', #11561, .T. ) ;
#10527=CARTESIAN_POINT ( 'NONE',  ( 1.500000000000001332, 0.000000000000000000, 0.000000000000000000 ) ) ;
#10545=ADVANCED_FACE ( 'NONE', ( #10725 ), #5141, .T. ) ;
#10547=DIRECTION ( 'NONE',  ( 0.000000000000000000, 0.000000000000000000, -1.000000000000000000 ) ) ;
#10586=MECHANICAL_DESIGN_GEOMETRIC_PRESENTATION_REPRESENTATION('',(#9156),#12693);
#10589=ORIENTED_EDGE ( 'NONE', *, *, #8777, .F. ) ;
#10597=ADVANCED_FACE ( 'NONE', ( #2332 ), #4078, .T. ) ;
#10656=ORIENTED_EDGE ( 'NONE', *, *, #17335, .T. ) ;
#10660=ADVANCED_FACE ( 'NONE', ( #1335 ), #19785, .F. ) ;
#10685=VERTEX_POINT ( 'NONE', #17916 ) ;
#10725=FACE_OUTER_BOUND ( 'NONE', #4297, .T. ) ;
#10775=ORIENTED_EDGE ( 'NONE', *, *, #4736, .F. ) ;
#10797=AXIS2_PLACEMENT_3D ( 'NONE', #10818, #2203, #17464 ) ;
#10818=CARTESIAN_POINT ( 'NONE',  ( -1.200000000000006617, 0.000000000000000000, 0.000000000000000000 ) ) ;
#10831=CARTESIAN_POINT ( 'NONE',  ( -1.500000000000001332, 0.000000000000000000, 0.000000000000000000 ) ) ;
#10859=TOROIDAL_SURFACE ( 'NONE', #12283, 5.633200000000004870, 0.02569999999999482421 ) ;
#10870=DIRECTION ( 'NONE',  ( 1.000000000000000000, 0.000000000000000000, 0.000000000000000000 ) ) ;
#10874=CARTESIAN_POINT ( 'NONE',  ( 1.399999999999998579, 0.000000000000000000, 0.000000000000000000 ) ) ;
#10888=ORIENTED_EDGE ( 'NONE', *, *, #19752, .F. ) ;
#10912=VECTOR ( 'NONE', #16645, 1000.000000000000114 ) ;
#10933=EDGE_LOOP ( 'NONE', ( #9402, #6671 ) ) ;
#10944=EDGE_CURVE ( 'NONE', #19543, #21459, #6469, .T. ) ;
#10963=SHAPE_DEFINITION_REPRESENTATION ( #9837, #10365 ) ;
#10977=CARTESIAN_POINT ( 'NONE',  ( -1.400000000000000577, 0.000000000000000000, 0.000000000000000000 ) ) ;
#11000=DIRECTION ( 'NONE',  ( 1.000000000000000000, 0.000000000000000000, 0.000000000000000000 ) ) ;
#11034=EDGE_LOOP ( 'NONE', ( #16038, #5800, #18302, #12187 ) ) ;
#11086=DIRECTION ( 'NONE',  ( 1.000000000000000000, -0.000000000000000000, -0.000000000000000000 ) ) ;
#11098=EDGE_LOOP ( 'NONE', ( #11676, #3848, #76, #4857 ) ) ;
#11105=CARTESIAN_POINT ( 'NONE',  ( -90.00000000000000000, 0.000000000000000000, -5.612499999999999822 ) ) ;
#11118=EDGE_LOOP ( 'NONE', ( #3529, #12354, #13744, #10095 ) ) ;
#11123=AXIS2_PLACEMENT_3D ( 'NONE', #7274, #3734, #5391 ) ;
#11149=FACE_BOUND ( 'NONE', #16718, .T. ) ;
#11193=DIRECTION ( 'NONE',  ( 0.000000000000000000, 1.224646799147355426E-16, 1.000000000000000000 ) ) ;
#11196=DIRECTION ( 'NONE',  ( 0.000000000000000000, 0.000000000000000000, -1.000000000000000000 ) ) ;
#11208=EDGE_LOOP ( 'NONE', ( #21080, #16194, #1867, #3596 ) ) ;
#11225=EDGE_CURVE ( 'NONE', #1128, #3829, #9997, .T. ) ;
#11226=CARTESIAN_POINT ( 'NONE',  ( 1.500000000000001332, 0.000000000000000000, 0.000000000000000000 ) ) ;
#11242=ADVANCED_FACE ( 'NONE', ( #20395 ), #10320, .F. ) ;
#11253=AXIS2_PLACEMENT_3D ( 'NONE', #21073, #2086, #18989 ) ;
#11288=DIRECTION ( 'NONE',  ( 0.000000000000000000, 1.224646799147353207E-16, 1.000000000000000000 ) ) ;
#11302=DIRECTION ( 'NONE',  ( 0.000000000000000000, 0.000000000000000000, -1.000000000000000000 ) ) ;
#11361=DIRECTION ( 'NONE',  ( 0.000000000000000000, -1.000000000000000000, 0.000000000000000000 ) ) ;
#11429=LINE ( 'NONE', #6473, #21662 ) ;
#11436=DIRECTION ( 'NONE',  ( 0.000000000000000000, 0.000000000000000000, -1.000000000000000000 ) ) ;
#11460=VECTOR ( 'NONE', #16438, 1000.000000000000000 ) ;
#11461=EDGE_LOOP ( 'NONE', ( #1589, #1810, #21317, #1653 ) ) ;
#11491=AXIS2_PLACEMENT_3D ( 'NONE', #19671, #4647, #16248 ) ;
#11500=ADVANCED_FACE ( 'NONE', ( #4460, #9412 ), #6357, .T. ) ;
#11523=DIRECTION ( 'NONE',  ( 0.000000000000000000, 0.000000000000000000, -1.000000000000000000 ) ) ;
#11547=ORIENTED_EDGE ( 'NONE', *, *, #7755, .T. ) ;
#11556=DIRECTION ( 'NONE',  ( 0.000000000000000000, 1.224646799147362821E-16, 1.000000000000000000 ) ) ;
#11561=EDGE_LOOP ( 'NONE', ( #13300, #6058, #21287, #217 ) ) ;
#11582=DIRECTION ( 'NONE',  ( 1.000000000000000000, -0.000000000000000000, -0.000000000000000000 ) ) ;
#11606=ORIENTED_EDGE ( 'NONE', *, *, #6699, .T. ) ;
#11615=CIRCLE ( 'NONE', #19367, 6.887500000000022382 ) ;
#11621=ORIENTED_EDGE ( 'NONE', *, *, #19058, .F. ) ;
#11656=CARTESIAN_POINT ( 'NONE',  ( -90.00000000000000000, 0.000000000000000000, 0.000000000000000000 ) ) ;
#11670=UNCERTAINTY_MEASURE_WITH_UNIT (LENGTH_MEASURE( 1.000000000000000082E-05 ), #16722, 'distance_accuracy_value', 'NONE');
#11676=ORIENTED_EDGE ( 'NONE', *, *, #9230, .F. ) ;
#11690=AXIS2_PLACEMENT_3D ( 'NONE', #6714, #13428, #20172 ) ;
#11694=DIRECTION ( 'NONE',  ( 0.000000000000000000, 0.000000000000000000, -1.000000000000000000 ) ) ;
#11702=DIRECTION ( 'NONE',  ( 0.000000000000000000, 1.224646799147355426E-16, 1.000000000000000000 ) ) ;
#11703=ORIENTED_EDGE ( 'NONE', *, *, #18226, .F. ) ;
#11710=DIRECTION ( 'NONE',  ( 0.000000000000000000, 0.000000000000000000, -1.000000000000000000 ) ) ;
#11724=VECTOR ( 'NONE', #17911, 1000.000000000000000 ) ;
#11740=EDGE_CURVE ( 'NONE', #7767, #6657, #134, .T. ) ;
#11741=EDGE_CURVE ( 'NONE', #15070, #20932, #13618, .T. ) ;
#11759=DIRECTION ( 'NONE',  ( 0.000000000000000000, 0.000000000000000000, -1.000000000000000000 ) ) ;
#11779=ORIENTED_EDGE ( 'NONE', *, *, #1103, .T. ) ;
#11789=DIRECTION ( 'NONE',  ( 1.000000000000000000, 0.000000000000000000, 0.000000000000000000 ) ) ;
#11799=AXIS2_PLACEMENT_3D ( 'NONE', #159, #1712, #5354 ) ;
#11810=CARTESIAN_POINT ( 'NONE',  ( 1.199999999999992628, 0.000000000000000000, -6.728125000000023448 ) ) ;
#11817=DIRECTION ( 'NONE',  ( 1.000000000000000000, 0.000000000000000000, 0.000000000000000000 ) ) ;
#11855=CARTESIAN_POINT ( 'NONE',  ( -1.200000000000006617, 8.434754829127421589E-16, 6.887500000000022382 ) ) ;
#11885=ORIENTED_EDGE ( 'NONE', *, *, #18292, .T. ) ;
#11925=ORIENTED_EDGE ( 'NONE', *, *, #248, .T. ) ;
#11959=VERTEX_POINT ( 'NONE', #20861 ) ;
#11977=ORIENTED_EDGE ( 'NONE', *, *, #17217, .T. ) ;
#11986=CARTESIAN_POINT ( 'NONE',  ( -90.00000000000000000, 6.873330160214519262E-16, 5.612499999999999822 ) ) ;
#11995=ORIENTED_EDGE ( 'NONE', *, *, #15930, .F. ) ;
#12015=DIRECTION ( 'NONE',  ( 0.000000000000000000, 0.000000000000000000, -1.000000000000000000 ) ) ;
#12049=ORIENTED_EDGE ( 'NONE', *, *, #20721, .F. ) ;
#12084=DIRECTION ( 'NONE',  ( 1.000000000000000000, -0.000000000000000000, -0.000000000000000000 ) ) ;
#12086=DIRECTION ( 'NONE',  ( 1.000000000000000000, 0.000000000000000000, 0.000000000000000000 ) ) ;
#12127=DIRECTION ( 'NONE',  ( 1.000000000000000000, 0.000000000000000000, 0.000000000000000000 ) ) ;
#12132=ORIENTED_EDGE ( 'NONE', *, *, #18283, .T. ) ;
#12149=AXIS2_PLACEMENT_3D ( 'NONE', #19806, #4336, #9405 ) ;
#12187=ORIENTED_EDGE ( 'NONE', *, *, #1472, .T. ) ;
#12188=EDGE_CURVE ( 'NONE', #3466, #20932, #18583, .T. ) ;
#12189=PRESENTATION_STYLE_ASSIGNMENT (( #17171 ) ) ;
#12196=AXIS2_PLACEMENT_3D ( 'NONE', #2461, #21020, #7439 ) ;
#12197=AXIS2_PLACEMENT_3D ( 'NONE', #5337, #10400, #7106 ) ;
#12216=EDGE_LOOP ( 'NONE', ( #19021, #15243, #2991, #19546 ) ) ;
#12234=DIRECTION ( 'NONE',  ( 0.000000000000000000, 0.000000000000000000, -1.000000000000000000 ) ) ;
#12248=DIRECTION ( 'NONE',  ( -0.000000000000000000, -1.000000000000000000, -0.000000000000000000 ) ) ;
#12254=CIRCLE ( 'NONE', #21436, 5.100000000000000533 ) ;
#12267=AXIS2_PLACEMENT_3D ( 'NONE', #4372, #11000, #19621 ) ;
#12283=AXIS2_PLACEMENT_3D ( 'NONE', #15398, #12084, #13754 ) ;
#12292=ADVANCED_FACE ( 'NONE', ( #14482, #16135 ), #7746, .T. ) ;
#12297=SURFACE_STYLE_FILL_AREA ( #14162 ) ;
#12308=DIRECTION ( 'NONE',  ( -1.000000000000000000, 0.000000000000000000, 0.000000000000000000 ) ) ;
#12339=CIRCLE ( 'NONE', #2816, 7.500000000000021316 ) ;
#12341=DIRECTION ( 'NONE',  ( 0.000000000000000000, 0.000000000000000000, -1.000000000000000000 ) ) ;
#12345=ADVANCED_FACE ( 'NONE', ( #18543 ), #18655, .F. ) ;
#12347=CARTESIAN_POINT ( 'NONE',  ( 1.500000000000001332, 0.000000000000000000, 0.000000000000000000 ) ) ;
#12354=ORIENTED_EDGE ( 'NONE', *, *, #9230, .T. ) ;
#12414=ADVANCED_FACE ( 'NONE', ( #5283 ), #16053, .T. ) ;
#12422=VERTEX_POINT ( 'NONE', #2273 ) ;
#12463=CONICAL_SURFACE ( 'NONE', #13886, 5.612499999999999822, 0.4883339510564123076 ) ;
#12469=FACE_OUTER_BOUND ( 'NONE', #19120, .T. ) ;
#12473=AXIS2_PLACEMENT_3D ( 'NONE', #250, #15374, #6996 ) ;
#12503=FILL_AREA_STYLE_COLOUR ( '', #1116 ) ;
#12521=ORIENTED_EDGE ( 'NONE', *, *, #2281, .T. ) ;
#12560=EDGE_CURVE ( 'NONE', #20636, #1054, #5832, .T. ) ;
#12578=CARTESIAN_POINT ( 'NONE',  ( -1.139999999999998570, 0.000000000000000000, 0.000000000000000000 ) ) ;
#12582=VECTOR ( 'NONE', #213, 1000.000000000000000 ) ;
#12588=VERTEX_POINT ( 'NONE', #16296 ) ;
#12658=EDGE_CURVE ( 'NONE', #4022, #1128, #17832, .T. ) ;
#12660=CIRCLE ( 'NONE', #11253, 0.02570000000000176310 ) ;
#12673=ORIENTED_EDGE ( 'NONE', *, *, #5730, .T. ) ;
#12693=( GEOMETRIC_REPRESENTATION_CONTEXT ( 3 ) GLOBAL_UNCERTAINTY_ASSIGNED_CONTEXT ( ( #12990 ) ) GLOBAL_UNIT_ASSIGNED_CONTEXT ( ( #1152, #4583, #2914 ) ) REPRESENTATION_CONTEXT ( 'NONE', 'WORKASPACE' ) );
#12747=DIRECTION ( 'NONE',  ( 0.000000000000000000, 0.000000000000000000, -1.000000000000000000 ) ) ;
#12782=CARTESIAN_POINT ( 'NONE',  ( 1.129531546211711479, 0.000000000000000000, 0.000000000000000000 ) ) ;
#12788=CYLINDRICAL_SURFACE ( 'NONE', #14365, 6.887500000000022382 ) ;
#12832=PRODUCT_CONTEXT ( 'NONE', #14335, 'mechanical' ) ;
#12849=ORIENTED_EDGE ( 'NONE', *, *, #3928, .F. ) ;
#12855=CIRCLE ( 'NONE', #20971, 6.728125000000023448 ) ;
#12865=CONICAL_SURFACE ( 'NONE', #6183, 5.612499999999999822, 0.4883339510564123076 ) ;
#12868=DIRECTION ( 'NONE',  ( 0.000000000000000000, 0.000000000000000000, -1.000000000000000000 ) ) ;
#12922=DIRECTION ( 'NONE',  ( 0.000000000000000000, 0.000000000000000000, -1.000000000000000000 ) ) ;
#12961=VECTOR ( 'NONE', #9315, 1000.000000000000114 ) ;
#12981=AXIS2_PLACEMENT_3D ( 'NONE', #10197, #8538, #2226 ) ;
#12990=UNCERTAINTY_MEASURE_WITH_UNIT (LENGTH_MEASURE( 1.000000000000000082E-05 ), #1152, 'distance_accuracy_value', 'NONE');
#13004=CARTESIAN_POINT ( 'NONE',  ( 1.500000000000001332, 0.000000000000000000, 0.000000000000000000 ) ) ;
#13016=EDGE_CURVE ( 'NONE', #6398, #14549, #6949, .T. ) ;
#13026=DIRECTION ( 'NONE',  ( 1.000000000000000000, 0.000000000000000000, 0.000000000000000000 ) ) ;
#13087=FACE_OUTER_BOUND ( 'NONE', #2764, .T. ) ;
#13117=DIRECTION ( 'NONE',  ( -0.8831157194574072999, 0.000000000000000000, 0.4691552259617553511 ) ) ;
#13122=CARTESIAN_POINT ( 'NONE',  ( -1.399999999999998579, 0.000000000000000000, -7.500000000000020428 ) ) ;
#13127=DIRECTION ( 'NONE',  ( 0.000000000000000000, 0.000000000000000000, -1.000000000000000000 ) ) ;
#13214=FACE_OUTER_BOUND ( 'NONE', #19969, .T. ) ;
#13244=EDGE_LOOP ( 'NONE', ( #15987, #14747 ) ) ;
#13300=ORIENTED_EDGE ( 'NONE', *, *, #248, .F. ) ;
#13312=CARTESIAN_POINT ( 'NONE',  ( 1.500000000000000888, 0.000000000000000000, -5.100000000000000533 ) ) ;
#13324=AXIS2_PLACEMENT_3D ( 'NONE', #7459, #17844, #12747 ) ;
#13339=DIRECTION ( 'NONE',  ( 1.000000000000000000, 0.000000000000000000, -0.000000000000000000 ) ) ;
#13406=COLOUR_RGB ( '', 0.31764706, 0.68627451, 0.89019608) ;
#13412=DIRECTION ( 'NONE',  ( 0.000000000000000000, 0.000000000000000000, -1.000000000000000000 ) ) ;
#13423=CARTESIAN_POINT ( 'NONE',  ( -1.200000000000006617, 0.000000000000000000, 0.000000000000000000 ) ) ;
#13428=DIRECTION ( 'NONE',  ( 1.000000000000000000, 0.000000000000000000, 0.000000000000000000 ) ) ;
#13431=CARTESIAN_POINT ( 'NONE',  ( 1.200000000000006617, 0.000000000000000000, 0.000000000000000000 ) ) ;
#13440=VERTEX_POINT ( 'NONE', #15920 ) ;
#13448=DIRECTION ( 'NONE',  ( -0.000000000000000000, 0.000000000000000000, -1.000000000000000000 ) ) ;
#13496=EDGE_CURVE ( 'NONE', #14549, #4382, #8295, .T. ) ;
#13521=DIRECTION ( 'NONE',  ( 0.000000000000000000, 0.000000000000000000, -1.000000000000000000 ) ) ;
#13536=ADVANCED_FACE ( 'NONE', ( #21224, #4429 ), #9597, .T. ) ;
#13561=DIRECTION ( 'NONE',  ( 0.000000000000000000, 0.000000000000000000, -1.000000000000000000 ) ) ;
#13605=DIRECTION ( 'NONE',  ( 1.000000000000000000, 0.000000000000000000, 0.000000000000000000 ) ) ;
#13618=CIRCLE ( 'NONE', #12197, 0.02569999999999482421 ) ;
#13634=DIRECTION ( 'NONE',  ( 0.000000000000000000, 1.000000000000000000, -1.224646799147353207E-16 ) ) ;
#13644=EDGE_CURVE ( 'NONE', #21459, #19543, #9064, .T. ) ;
#13665=AXIS2_PLACEMENT_3D ( 'NONE', #20452, #8511, #10373 ) ;
#13677=VECTOR ( 'NONE', #7371, 1000.000000000000000 ) ;
#13693=CARTESIAN_POINT ( 'NONE',  ( 1.199999999999998845, 6.728125000000023448, 0.000000000000000000 ) ) ;
#13744=ORIENTED_EDGE ( 'NONE', *, *, #10944, .T. ) ;
#13754=DIRECTION ( 'NONE',  ( 0.000000000000000000, 0.000000000000000000, -1.000000000000000000 ) ) ;
#13757=DIRECTION ( 'NONE',  ( 1.000000000000000000, 0.000000000000000000, 0.000000000000000000 ) ) ;
#13767=EDGE_CURVE ( 'NONE', #20636, #20241, #20718, .T. ) ;
#13819=VERTEX_POINT ( 'NONE', #4190 ) ;
#13843=SHAPE_REPRESENTATION_RELATIONSHIP ( 'NONE' , 'NONE' ,  #10365, #4298 ) ;
#13847=ORIENTED_EDGE ( 'NONE', *, *, #14050, .F. ) ;
#13868=VERTEX_POINT ( 'NONE', #8166 ) ;
#13886=AXIS2_PLACEMENT_3D ( 'NONE', #2012, #247, #8533 ) ;
#13905=AXIS2_PLACEMENT_3D ( 'NONE', #20599, #15188, #3588 ) ;
#13925=ORIENTED_EDGE ( 'NONE', *, *, #1748, .F. ) ;
#13943=CIRCLE ( 'NONE', #3359, 7.400000000000019895 ) ;
#13973=CARTESIAN_POINT ( 'NONE',  ( 1.139999999999998570, 0.000000000000000000, 0.000000000000000000 ) ) ;
#13978=ORIENTED_EDGE ( 'NONE', *, *, #12188, .F. ) ;
#13988=CARTESIAN_POINT ( 'NONE',  ( -90.00000000000000000, 9.184850993605175555E-16, 7.500000000000020428 ) ) ;
#14014=CARTESIAN_POINT ( 'NONE',  ( -1.129531546211690385, 0.000000000000000000, 0.000000000000000000 ) ) ;
#14026=CARTESIAN_POINT ( 'NONE',  ( -1.140000000000000124, 0.000000000000000000, -5.633200000000004870 ) ) ;
#14029=EDGE_LOOP ( 'NONE', ( #5536, #13925 ) ) ;
#14050=EDGE_CURVE ( 'NONE', #6777, #3829, #5555, .T. ) ;
#14065=CIRCLE ( 'NONE', #14787, 0.09999999999999939493 ) ;
#14102=AXIS2_PLACEMENT_3D ( 'NONE', #19916, #30, #11523 ) ;
#14127=DIRECTION ( 'NONE',  ( 0.000000000000000000, 0.000000000000000000, -1.000000000000000000 ) ) ;
#14132=DIRECTION ( 'NONE',  ( 1.000000000000000000, -0.000000000000000000, -0.000000000000000000 ) ) ;
#14134=ADVANCED_FACE ( 'NONE', ( #10021 ), #21096, .T. ) ;
#14143=CARTESIAN_POINT ( 'NONE',  ( 1.129531546211678616, 0.000000000000000000, 0.000000000000000000 ) ) ;
#14147=DIRECTION ( 'NONE',  ( 0.000000000000000000, 0.000000000000000000, -1.000000000000000000 ) ) ;
#14153=EDGE_CURVE ( 'NONE', #6657, #7767, #12254, .T. ) ;
#14162=FILL_AREA_STYLE ('',( #12503 ) ) ;
#14164=DIRECTION ( 'NONE',  ( 1.000000000000000000, 0.000000000000000000, 0.000000000000000000 ) ) ;
#14185=DIRECTION ( 'NONE',  ( 1.000000000000000000, 0.000000000000000000, 0.000000000000000000 ) ) ;
#14205=EDGE_CURVE ( 'NONE', #12588, #6398, #16506, .T. ) ;
#14250=EDGE_LOOP ( 'NONE', ( #9450, #19744 ) ) ;
#14285=AXIS2_PLACEMENT_3D ( 'NONE', #20521, #15545, #2170 ) ;
#14300=CIRCLE ( 'NONE', #7954, 5.612499999999999822 ) ;
#14307=EDGE_CURVE ( 'NONE', #18258, #10685, #295, .T. ) ;
#14312=ORIENTED_EDGE ( 'NONE', *, *, #14307, .F. ) ;
#14335=APPLICATION_CONTEXT ( 'automotive_design' ) ;
#14341=ORIENTED_EDGE ( 'NONE', *, *, #420, .T. ) ;
#14365=AXIS2_PLACEMENT_3D ( 'NONE', #4407, #4194, #19536 ) ;
#14380=CIRCLE ( 'NONE', #20038, 6.887500000000022382 ) ;
#14385=ORIENTED_EDGE ( 'NONE', *, *, #9984, .F. ) ;
#14410=SURFACE_STYLE_USAGE ( .BOTH. , #7675 ) ;
#14432=CIRCLE ( 'NONE', #7735, 5.612499999999999822 ) ;
#14440=VERTEX_POINT ( 'NONE', #14840 ) ;
#14443=CARTESIAN_POINT ( 'NONE',  ( -90.00000000000000000, 0.000000000000000000, -5.612499999999999822 ) ) ;
#14445=PLANE ( 'NONE',  #9180 ) ;
#14450=AXIS2_PLACEMENT_3D ( 'NONE', #2585, #4254, #19392 ) ;
#14466=EDGE_CURVE ( 'NONE', #4022, #6777, #2059, .T. ) ;
#14475=ORIENTED_EDGE ( 'NONE', *, *, #9726, .F. ) ;
#14478=ORIENTED_EDGE ( 'NONE', *, *, #11225, .F. ) ;
#14482=FACE_OUTER_BOUND ( 'NONE', #2950, .T. ) ;
#14549=VERTEX_POINT ( 'NONE', #8859 ) ;
#14552=VERTEX_POINT ( 'NONE', #11855 ) ;
#14554=ORIENTED_EDGE ( 'NONE', *, *, #17717, .T. ) ;
#14565=PLANE ( 'NONE',  #16186 ) ;
#14604=ORIENTED_EDGE ( 'NONE', *, *, #9365, .F. ) ;
#14608=FACE_OUTER_BOUND ( 'NONE', #6274, .T. ) ;
#14625=CIRCLE ( 'NONE', #172, 5.612499999999999822 ) ;
#14649=ORIENTED_EDGE ( 'NONE', *, *, #712, .F. ) ;
#14671=AXIS2_PLACEMENT_3D ( 'NONE', #13973, #8989, #10547 ) ;
#14697=TOROIDAL_SURFACE ( 'NONE', #18932, 6.866799999999992465, 0.02570000000000154800 ) ;
#14736=AXIS2_PLACEMENT_3D ( 'NONE', #313, #18759, #20098 ) ;
#14747=ORIENTED_EDGE ( 'NONE', *, *, #16209, .T. ) ;
#14787=AXIS2_PLACEMENT_3D ( 'NONE', #7607, #20974, #15780 ) ;
#14840=CARTESIAN_POINT ( 'NONE',  ( -1.200000000000006617, 6.873330160214519262E-16, 5.612499999999999822 ) ) ;
#14853=EDGE_LOOP ( 'NONE', ( #1242, #21160, #5840, #14341 ) ) ;
#14891=CARTESIAN_POINT ( 'NONE',  ( -90.00000000000000000, 0.000000000000000000, 0.000000000000000000 ) ) ;
#14892=DIRECTION ( 'NONE',  ( 0.000000000000000000, 0.000000000000000000, -1.000000000000000000 ) ) ;
#14893=CARTESIAN_POINT ( 'NONE',  ( -1.399999999999998579, 0.000000000000000000, 0.000000000000000000 ) ) ;
#14917=DIRECTION ( 'NONE',  ( 1.000000000000000000, 0.000000000000000000, 0.000000000000000000 ) ) ;
#14928=CARTESIAN_POINT ( 'NONE',  ( 1.199999999999992628, 0.000000000000000000, -6.887500000000022382 ) ) ;
#14946=CIRCLE ( 'NONE', #6151, 7.400000000000020783 ) ;
#14951=DIRECTION ( 'NONE',  ( 1.000000000000000000, 0.000000000000000000, 0.000000000000000000 ) ) ;
#14955=DIRECTION ( 'NONE',  ( 1.000000000000000000, -0.000000000000000000, -0.000000000000000000 ) ) ;
#14979=CARTESIAN_POINT ( 'NONE',  ( -1.139999999999998570, 8.422079734756228398E-16, 6.866799999999992465 ) ) ;
#14995=CARTESIAN_POINT ( 'NONE',  ( -1.399999999999998579, 0.000000000000000000, 0.000000000000000000 ) ) ;
#15025=ADVANCED_FACE ( 'NONE', ( #12469 ), #19215, .F. ) ;
#15070=VERTEX_POINT ( 'NONE', #3971 ) ;
#15078=FACE_OUTER_BOUND ( 'NONE', #20380, .T. ) ;
#15091=CIRCLE ( 'NONE', #12267, 5.100000000000000533 ) ;
#15093=AXIS2_PLACEMENT_3D ( 'NONE', #20924, #10870, #8002 ) ;
#15114=DIRECTION ( 'NONE',  ( 0.000000000000000000, 0.000000000000000000, -1.000000000000000000 ) ) ;
#15129=CARTESIAN_POINT ( 'NONE',  ( -90.00000000000000000, 0.000000000000000000, 0.000000000000000000 ) ) ;
#15151=ADVANCED_FACE ( 'NONE', ( #16233, #11149 ), #14565, .T. ) ;
#15172=CARTESIAN_POINT ( 'NONE',  ( 1.200000000000006617, 0.000000000000000000, 0.000000000000000000 ) ) ;
#15188=DIRECTION ( 'NONE',  ( 1.000000000000000000, 0.000000000000000000, 0.000000000000000000 ) ) ;
#15216=DIRECTION ( 'NONE',  ( 0.000000000000000000, 0.000000000000000000, 1.000000000000000000 ) ) ;
#15217=CARTESIAN_POINT ( 'NONE',  ( 1.500000000000001332, 0.000000000000000000, 0.000000000000000000 ) ) ;
#15243=ORIENTED_EDGE ( 'NONE', *, *, #9411, .T. ) ;
#15283=DIRECTION ( 'NONE',  ( 1.000000000000000000, -0.000000000000000000, -0.000000000000000000 ) ) ;
#15302=AXIS2_PLACEMENT_3D ( 'NONE', #16728, #15283, #20056 ) ;
#15304=DIRECTION ( 'NONE',  ( 0.000000000000000000, 0.000000000000000000, -1.000000000000000000 ) ) ;
#15337=FACE_OUTER_BOUND ( 'NONE', #7388, .T. ) ;
#15374=DIRECTION ( 'NONE',  ( 1.000000000000000000, 0.000000000000000000, 0.000000000000000000 ) ) ;
#15398=CARTESIAN_POINT ( 'NONE',  ( 1.114299999999999846, 0.000000000000000000, 0.000000000000000000 ) ) ;
#15409=AXIS2_PLACEMENT_3D ( 'NONE', #18361, #4649, #21325 ) ;
#15481=DIRECTION ( 'NONE',  ( 0.000000000000000000, 0.000000000000000000, 1.000000000000000000 ) ) ;
#15486=CARTESIAN_POINT ( 'NONE',  ( -1.399999999999999911, 0.000000000000000000, 0.000000000000000000 ) ) ;
#15545=DIRECTION ( 'NONE',  ( 1.000000000000000000, 0.000000000000000000, 0.000000000000000000 ) ) ;
#15552=CARTESIAN_POINT ( 'NONE',  ( -1.500000000000001332, 0.000000000000000000, 0.000000000000000000 ) ) ;
#15557=DIRECTION ( 'NONE',  ( 0.000000000000000000, 0.000000000000000000, -1.000000000000000000 ) ) ;
#15567=AXIS2_PLACEMENT_3D ( 'NONE', #21837, #20187, #17085 ) ;
#15571=DIRECTION ( 'NONE',  ( 1.000000000000000000, -0.000000000000000000, -0.000000000000000000 ) ) ;
#15576=EDGE_LOOP ( 'NONE', ( #11779, #1709 ) ) ;
#15597=CARTESIAN_POINT ( 'NONE',  ( -1.399999999999998579, 6.184466335694134054E-16, 5.000000000000000888 ) ) ;
#15629=CYLINDRICAL_SURFACE ( 'NONE', #14450, 5.612499999999999822 ) ;
#15674=CIRCLE ( 'NONE', #4386, 0.02569999999999482421 ) ;
#15677=CARTESIAN_POINT ( 'NONE',  ( -1.200000000000006617, 0.000000000000000000, 0.000000000000000000 ) ) ;
#15712=CIRCLE ( 'NONE', #11123, 6.728125000000023448 ) ;
#15724=( NAMED_UNIT ( * ) SI_UNIT ( $, .STERADIAN. ) SOLID_ANGLE_UNIT ( ) );
#15754=DIRECTION ( 'NONE',  ( 1.000000000000000000, 0.000000000000000000, 0.000000000000000000 ) ) ;
#15755=CARTESIAN_POINT ( 'NONE',  ( -1.139999999999998570, 0.000000000000000000, 0.000000000000000000 ) ) ;
#15760=DIRECTION ( 'NONE',  ( 0.000000000000000000, 0.000000000000000000, -1.000000000000000000 ) ) ;
#15780=DIRECTION ( 'NONE',  ( 0.000000000000000000, 1.224646799147353947E-16, 1.000000000000000000 ) ) ;
#15805=ORIENTED_EDGE ( 'NONE', *, *, #1748, .T. ) ;
#15811=EDGE_CURVE ( 'NONE', #10685, #18258, #12339, .T. ) ;
#15889=DIRECTION ( 'NONE',  ( -1.000000000000000000, -0.000000000000000000, -0.000000000000000000 ) ) ;
#15890=ORIENTED_EDGE ( 'NONE', *, *, #5321, .T. ) ;
#15920=CARTESIAN_POINT ( 'NONE',  ( -1.500000000000000444, 0.000000000000000000, -5.100000000000000533 ) ) ;
#15930=EDGE_CURVE ( 'NONE', #20932, #3466, #2979, .T. ) ;
#15949=CIRCLE ( 'NONE', #5025, 0.1000000000000002554 ) ;
#15961=ORIENTED_EDGE ( 'NONE', *, *, #6542, .T. ) ;
#15982=FACE_OUTER_BOUND ( 'NONE', #20963, .T. ) ;
#15987=ORIENTED_EDGE ( 'NONE', *, *, #5392, .T. ) ;
#16007=VECTOR ( 'NONE', #17971, 1000.000000000000000 ) ;
#16031=TOROIDAL_SURFACE ( 'NONE', #10389, 7.400000000000020783, 0.1000000000000001582 ) ;
#16033=AXIS2_PLACEMENT_3D ( 'NONE', #3690, #17066, #1923 ) ;
#16038=ORIENTED_EDGE ( 'NONE', *, *, #6796, .F. ) ;
#16053=TOROIDAL_SURFACE ( 'NONE', #21705, 5.633200000000004870, 0.02570000000000143697 ) ;
#16108=ORIENTED_EDGE ( 'NONE', *, *, #7209, .T. ) ;
#16117=CARTESIAN_POINT ( 'NONE',  ( -90.00000000000000000, 0.000000000000000000, 0.000000000000000000 ) ) ;
#16119=CIRCLE ( 'NONE', #631, 5.612499999999999822 ) ;
#16131=AXIS2_PLACEMENT_3D ( 'NONE', #15755, #4262, #12868 ) ;
#16135=FACE_BOUND ( 'NONE', #6257, .T. ) ;
#16137=DIRECTION ( 'NONE',  ( 1.000000000000000000, 0.000000000000000000, 0.000000000000000000 ) ) ;
#16176=ORIENTED_EDGE ( 'NONE', *, *, #452, .T. ) ;
#16181=FILL_AREA_STYLE_COLOUR ( '', #13406 ) ;
#16186=AXIS2_PLACEMENT_3D ( 'NONE', #4408, #6186, #6518 ) ;
#16194=ORIENTED_EDGE ( 'NONE', *, *, #288, .T. ) ;
#16199=DIRECTION ( 'NONE',  ( 1.000000000000000000, -0.000000000000000000, -0.000000000000000000 ) ) ;
#16202=CONICAL_SURFACE ( 'NONE', #3491, 5.453125000000000000, 0.4883339510564123076 ) ;
#16203=VERTEX_POINT ( 'NONE', #17364 ) ;
#16209=EDGE_CURVE ( 'NONE', #826, #4912, #18875, .T. ) ;
#16233=FACE_OUTER_BOUND ( 'NONE', #190, .T. ) ;
#16248=DIRECTION ( 'NONE',  ( 0.000000000000000000, 0.000000000000000000, -1.000000000000000000 ) ) ;
#16289=ORIENTED_EDGE ( 'NONE', *, *, #19314, .F. ) ;
#16293=AXIS2_PLACEMENT_3D ( 'NONE', #12782, #755, #7498 ) ;
#16296=CARTESIAN_POINT ( 'NONE',  ( 1.139999999999995017, 0.000000000000000000, -5.633200000000004870 ) ) ;
#16331=AXIS2_PLACEMENT_3D ( 'NONE', #1479, #14955, #20053 ) ;
#16337=AXIS2_PLACEMENT_3D ( 'NONE', #14893, #4958, #11694 ) ;
#16364=ADVANCED_FACE ( 'NONE', ( #10251 ), #19567, .T. ) ;
#16366=VECTOR ( 'NONE', #12086, 1000.000000000000000 ) ;
#16373=VECTOR ( 'NONE', #20736, 1000.000000000000000 ) ;
#16420=ORIENTED_EDGE ( 'NONE', *, *, #5321, .F. ) ;
#16428=ADVANCED_FACE ( 'NONE', ( #2083 ), #12865, .T. ) ;
#16438=DIRECTION ( 'NONE',  ( 1.000000000000000000, 0.000000000000000000, 0.000000000000000000 ) ) ;
#16460=DIRECTION ( 'NONE',  ( 0.000000000000000000, 0.000000000000000000, -1.000000000000000000 ) ) ;
#16482=EDGE_CURVE ( 'NONE', #18882, #769, #15712, .T. ) ;
#16501=EDGE_CURVE ( 'NONE', #6777, #4022, #13943, .T. ) ;
#16506=CIRCLE ( 'NONE', #19325, 5.633200000000004870 ) ;
#16566=CARTESIAN_POINT ( 'NONE',  ( -1.114300000000000290, 0.000000000000000000, 0.000000000000000000 ) ) ;
#16570=ORIENTED_EDGE ( 'NONE', *, *, #8904, .F. ) ;
#16583=CARTESIAN_POINT ( 'NONE',  ( 1.139999999999998570, 8.422079734756228398E-16, 6.866799999999992465 ) ) ;
#16616=ORIENTED_EDGE ( 'NONE', *, *, #12658, .T. ) ;
#16644=ORIENTED_EDGE ( 'NONE', *, *, #8647, .F. ) ;
#16645=DIRECTION ( 'NONE',  ( 0.8831157194574072999, 0.000000000000000000, -0.4691552259617553511 ) ) ;
#16655=DIRECTION ( 'NONE',  ( 1.000000000000000000, 0.000000000000000000, 0.000000000000000000 ) ) ;
#16659=CARTESIAN_POINT ( 'NONE',  ( -1.129531546211723025, 0.000000000000000000, -5.612499999999999822 ) ) ;
#16661=DIRECTION ( 'NONE',  ( 1.000000000000000000, 0.000000000000000000, 0.000000000000000000 ) ) ;
#16665=EDGE_CURVE ( 'NONE', #16727, #4382, #5850, .T. ) ;
#16685=ORIENTED_EDGE ( 'NONE', *, *, #5392, .F. ) ;
#16699=EDGE_LOOP ( 'NONE', ( #19285, #4055, #9704, #14478 ) ) ;
#16718=EDGE_LOOP ( 'NONE', ( #10589, #2971 ) ) ;
#16722=( LENGTH_UNIT ( ) NAMED_UNIT ( * ) SI_UNIT ( .MILLI., .METRE. ) );
#16727=VERTEX_POINT ( 'NONE', #8032 ) ;
#16728=CARTESIAN_POINT ( 'NONE',  ( -1.114300000000000068, 0.000000000000000000, 0.000000000000000000 ) ) ;
#16746=CIRCLE ( 'NONE', #5808, 6.728125000000022560 ) ;
#16762=ORIENTED_EDGE ( 'NONE', *, *, #15930, .T. ) ;
#16784=DIRECTION ( 'NONE',  ( 0.000000000000000000, 0.000000000000000000, -1.000000000000000000 ) ) ;
#16790=VERTEX_POINT ( 'NONE', #4496 ) ;
#16819=AXIS2_PLACEMENT_3D ( 'NONE', #20323, #1320, #4738 ) ;
#16873=PLANE ( 'NONE',  #4360 ) ;
#16891=CARTESIAN_POINT ( 'NONE',  ( -1.200000000000006617, 0.000000000000000000, 0.000000000000000000 ) ) ;
#16909=ORIENTED_EDGE ( 'NONE', *, *, #20622, .T. ) ;
#16923=DIRECTION ( 'NONE',  ( 0.000000000000000000, 0.000000000000000000, -1.000000000000000000 ) ) ;
#16964=DIRECTION ( 'NONE',  ( 0.000000000000000000, 0.000000000000000000, -1.000000000000000000 ) ) ;
#16972=ORIENTED_EDGE ( 'NONE', *, *, #20431, .T. ) ;
#16981=ORIENTED_EDGE ( 'NONE', *, *, #19982, .T. ) ;
#16989=CARTESIAN_POINT ( 'NONE',  ( -1.114300000000000068, 0.000000000000000000, 0.000000000000000000 ) ) ;
#17003=ORIENTED_EDGE ( 'NONE', *, *, #8777, .T. ) ;
#17005=CYLINDRICAL_SURFACE ( 'NONE', #16819, 6.887500000000022382 ) ;
#17027=VECTOR ( 'NONE', #11817, 1000.000000000000000 ) ;
#17054=VERTEX_POINT ( 'NONE', #17700 ) ;
#17066=DIRECTION ( 'NONE',  ( 1.000000000000000000, 0.000000000000000000, 0.000000000000000000 ) ) ;
#17069=LINE ( 'NONE', #11986, #16366 ) ;
#17085=DIRECTION ( 'NONE',  ( 1.000000000000000000, 0.000000000000000000, 0.000000000000000000 ) ) ;
#17090=CARTESIAN_POINT ( 'NONE',  ( 1.500000000000000000, 5.100000000000000533, 0.000000000000000000 ) ) ;
#17104=DIRECTION ( 'NONE',  ( 1.000000000000000000, 0.000000000000000000, 0.000000000000000000 ) ) ;
#17109=EDGE_LOOP ( 'NONE', ( #21483, #18143 ) ) ;
#17126=PRODUCT_DEFINITION_CONTEXT ( 'detailed design', #774, 'design' ) ;
#17130=DIRECTION ( 'NONE',  ( 1.000000000000000000, 0.000000000000000000, 0.000000000000000000 ) ) ;
#17142=AXIS2_PLACEMENT_3D ( 'NONE', #15486, #7424, #14147 ) ;
#17168=ORIENTED_EDGE ( 'NONE', *, *, #3928, .T. ) ;
#17171=SURFACE_STYLE_USAGE ( .BOTH. , #10416 ) ;
#17202=ORIENTED_EDGE ( 'NONE', *, *, #20721, .T. ) ;
#17217=EDGE_CURVE ( 'NONE', #6557, #17273, #9735, .T. ) ;
#17226=FACE_OUTER_BOUND ( 'NONE', #2217, .T. ) ;
#17273=VERTEX_POINT ( 'NONE', #10278 ) ;
#17309=VERTEX_POINT ( 'NONE', #14026 ) ;
#17335=EDGE_CURVE ( 'NONE', #14552, #18616, #17867, .T. ) ;
#17364=CARTESIAN_POINT ( 'NONE',  ( 1.399999999999998579, 6.123233995736766282E-16, 5.000000000000000000 ) ) ;
#17403=CARTESIAN_POINT ( 'NONE',  ( 1.114299999999999846, 0.000000000000000000, 0.000000000000000000 ) ) ;
#17416=CIRCLE ( 'NONE', #2580, 5.100000000000000533 ) ;
#17441=EDGE_CURVE ( 'NONE', #4912, #12422, #19330, .T. ) ;
#17464=DIRECTION ( 'NONE',  ( 0.000000000000000000, 0.000000000000000000, -1.000000000000000000 ) ) ;
#17495=AXIS2_PLACEMENT_3D ( 'NONE', #3885, #21005, #9170 ) ;
#17539=EDGE_CURVE ( 'NONE', #2562, #9461, #1304, .T. ) ;
#17544=CARTESIAN_POINT ( 'NONE',  ( -1.200000000000006617, 0.000000000000000000, -5.612499999999999822 ) ) ;
#17564=ADVANCED_FACE ( 'NONE', ( #6632 ), #14697, .T. ) ;
#17581=ORIENTED_EDGE ( 'NONE', *, *, #3952, .F. ) ;
#17582=EDGE_CURVE ( 'NONE', #6657, #17054, #948, .T. ) ;
#17600=CARTESIAN_POINT ( 'NONE',  ( -1.200000000000006617, 0.000000000000000000, -6.887500000000022382 ) ) ;
#17601=ADVANCED_FACE ( 'NONE', ( #8171 ), #17005, .F. ) ;
#17659=DIRECTION ( 'NONE',  ( 1.000000000000000000, 0.000000000000000000, 0.000000000000000000 ) ) ;
#17699=EDGE_CURVE ( 'NONE', #769, #18882, #9751, .T. ) ;
#17700=CARTESIAN_POINT ( 'NONE',  ( 1.399999999999998579, 0.000000000000000000, -5.000000000000000000 ) ) ;
#17717=EDGE_CURVE ( 'NONE', #18616, #6321, #20534, .T. ) ;
#17782=DIRECTION ( 'NONE',  ( 0.000000000000000000, 0.000000000000000000, -1.000000000000000000 ) ) ;
#17787=CIRCLE ( 'NONE', #8267, 0.1000000000000002554 ) ;
#17814=CARTESIAN_POINT ( 'NONE',  ( 1.129531546211711479, 0.000000000000000000, -5.612499999999999822 ) ) ;
#17815=ORIENTED_EDGE ( 'NONE', *, *, #16665, .T. ) ;
#17832=CIRCLE ( 'NONE', #1600, 0.1000000000000002554 ) ;
#17844=DIRECTION ( 'NONE',  ( -1.000000000000000000, 0.000000000000000000, 0.000000000000000000 ) ) ;
#17867=CIRCLE ( 'NONE', #10797, 6.887500000000022382 ) ;
#17911=DIRECTION ( 'NONE',  ( 1.000000000000000000, 0.000000000000000000, 0.000000000000000000 ) ) ;
#17916=CARTESIAN_POINT ( 'NONE',  ( 1.399999999999998579, 0.000000000000000000, -7.500000000000021316 ) ) ;
#17927=CARTESIAN_POINT ( 'NONE',  ( 1.400000000000000133, 6.245698675651501825E-16, 5.100000000000000533 ) ) ;
#17953=ORIENTED_EDGE ( 'NONE', *, *, #17582, .F. ) ;
#17955=VERTEX_POINT ( 'NONE', #17544 ) ;
#17971=DIRECTION ( 'NONE',  ( 1.000000000000000000, 0.000000000000000000, 0.000000000000000000 ) ) ;
#17996=EDGE_LOOP ( 'NONE', ( #19815, #4825, #8605, #7714 ) ) ;
#18058=ORIENTED_EDGE ( 'NONE', *, *, #8413, .T. ) ;
#18075=DIRECTION ( 'NONE',  ( 1.000000000000000000, 0.000000000000000000, 0.000000000000000000 ) ) ;
#18083=ADVANCED_FACE ( 'NONE', ( #18423 ), #5214, .T. ) ;
#18086=ORIENTED_EDGE ( 'NONE', *, *, #452, .F. ) ;
#18089=FACE_OUTER_BOUND ( 'NONE', #3413, .T. ) ;
#18143=ORIENTED_EDGE ( 'NONE', *, *, #11740, .F. ) ;
#18157=DIRECTION ( 'NONE',  ( 0.000000000000000000, -1.000000000000000000, 0.000000000000000000 ) ) ;
#18184=CARTESIAN_POINT ( 'NONE',  ( -1.399999999999999911, 0.000000000000000000, 0.000000000000000000 ) ) ;
#18186=AXIS2_PLACEMENT_3D ( 'NONE', #19294, #9333, #7801 ) ;
#18195=TOROIDAL_SURFACE ( 'NONE', #9009, 5.100000000000000533, 0.09999999999999971412 ) ;
#18202=CIRCLE ( 'NONE', #12196, 0.02570000000000176310 ) ;
#18226=EDGE_CURVE ( 'NONE', #16203, #17054, #273, .T. ) ;
#18230=DIRECTION ( 'NONE',  ( 0.000000000000000000, 0.000000000000000000, -1.000000000000000000 ) ) ;
#18246=AXIS2_PLACEMENT_3D ( 'NONE', #1875, #7086, #3867 ) ;
#18252=VECTOR ( 'NONE', #14917, 1000.000000000000000 ) ;
#18258=VERTEX_POINT ( 'NONE', #2258 ) ;
#18279=CIRCLE ( 'NONE', #16131, 5.633200000000004870 ) ;
#18283=EDGE_CURVE ( 'NONE', #13819, #6262, #5554, .T. ) ;
#18292=EDGE_CURVE ( 'NONE', #8785, #14440, #2582, .T. ) ;
#18302=ORIENTED_EDGE ( 'NONE', *, *, #19058, .T. ) ;
#18323=CARTESIAN_POINT ( 'NONE',  ( -1.200000000000006617, 0.000000000000000000, 0.000000000000000000 ) ) ;
#18361=CARTESIAN_POINT ( 'NONE',  ( -1.500000000000000000, 5.453125000000000000, 0.000000000000000000 ) ) ;
#18402=DIRECTION ( 'NONE',  ( 0.000000000000000000, 0.000000000000000000, -1.000000000000000000 ) ) ;
#18409=DIRECTION ( 'NONE',  ( 0.000000000000000000, 0.000000000000000000, -1.000000000000000000 ) ) ;
#18423=FACE_OUTER_BOUND ( 'NONE', #1340, .T. ) ;
#18448=DIRECTION ( 'NONE',  ( 0.000000000000000000, 1.000000000000000000, -1.224646799147353207E-16 ) ) ;
#18469=ORIENTED_EDGE ( 'NONE', *, *, #13644, .F. ) ;
#18479=EDGE_LOOP ( 'NONE', ( #5169, #19064, #1881, #13978 ) ) ;
#18489=ORIENTED_EDGE ( 'NONE', *, *, #8576, .F. ) ;
#18543=FACE_OUTER_BOUND ( 'NONE', #7741, .T. ) ;
#18555=DIRECTION ( 'NONE',  ( 1.000000000000000000, -0.000000000000000000, -0.000000000000000000 ) ) ;
#18573=LINE ( 'NONE', #4751, #17027 ) ;
#18583=CIRCLE ( 'NONE', #21741, 6.866799999999992465 ) ;
#18602=ORIENTED_EDGE ( 'NONE', *, *, #11740, .T. ) ;
#18616=VERTEX_POINT ( 'NONE', #17600 ) ;
#18624=AXIS2_PLACEMENT_3D ( 'NONE', #17403, #3595, #15304 ) ;
#18628=DIRECTION ( 'NONE',  ( 0.000000000000000000, 0.000000000000000000, -1.000000000000000000 ) ) ;
#18655=CYLINDRICAL_SURFACE ( 'NONE', #14285, 6.728125000000022560 ) ;
#18666=DIRECTION ( 'NONE',  ( 1.000000000000000000, 0.000000000000000000, 0.000000000000000000 ) ) ;
#18679=CIRCLE ( 'NONE', #3841, 0.02569999999999482421 ) ;
#18734=FACE_OUTER_BOUND ( 'NONE', #7414, .T. ) ;
#18749=FACE_OUTER_BOUND ( 'NONE', #10933, .T. ) ;
#18755=CARTESIAN_POINT ( 'NONE',  ( -1.129531546211690385, 0.000000000000000000, -6.887500000000022382 ) ) ;
#18759=DIRECTION ( 'NONE',  ( 0.000000000000000000, -1.000000000000000000, 0.000000000000000000 ) ) ;
#18761=MECHANICAL_DESIGN_GEOMETRIC_PRESENTATION_REPRESENTATION('',(#2519),#3582);
#18765=EDGE_CURVE ( 'NONE', #17309, #16790, #6682, .T. ) ;
#18766=CARTESIAN_POINT ( 'NONE',  ( -90.00000000000000000, 0.000000000000000000, -6.887500000000022382 ) ) ;
#18781=EDGE_CURVE ( 'NONE', #7767, #16203, #9111, .T. ) ;
#18816=CIRCLE ( 'NONE', #1524, 5.453125000000000000 ) ;
#18824=ORIENTED_EDGE ( 'NONE', *, *, #1472, .F. ) ;
#18833=AXIS2_PLACEMENT_3D ( 'NONE', #10240, #11789, #20516 ) ;
#18836=FACE_OUTER_BOUND ( 'NONE', #7899, .T. ) ;
#18875=CIRCLE ( 'NONE', #21686, 6.728125000000022560 ) ;
#18882=VERTEX_POINT ( 'NONE', #11810 ) ;
#18886=LINE ( 'NONE', #3629, #20441 ) ;
#18932=AXIS2_PLACEMENT_3D ( 'NONE', #16566, #18555, #15114 ) ;
#18935=ORIENTED_EDGE ( 'NONE', *, *, #9205, .T. ) ;
#18989=DIRECTION ( 'NONE',  ( 0.000000000000000000, 1.224646799147324364E-16, 1.000000000000000000 ) ) ;
#19014=AXIS2_PLACEMENT_3D ( 'NONE', #17927, #1235, #11288 ) ;
#19015=ORIENTED_EDGE ( 'NONE', *, *, #8647, .T. ) ;
#19021=ORIENTED_EDGE ( 'NONE', *, *, #17335, .F. ) ;
#19053=CARTESIAN_POINT ( 'NONE',  ( -1.129531546211723025, 0.000000000000000000, 0.000000000000000000 ) ) ;
#19058=EDGE_CURVE ( 'NONE', #17955, #6262, #19749, .T. ) ;
#19064=ORIENTED_EDGE ( 'NONE', *, *, #4313, .T. ) ;
#19120=EDGE_LOOP ( 'NONE', ( #5107, #16685, #5189, #16108 ) ) ;
#19160=ADVANCED_FACE ( 'NONE', ( #18089 ), #16202, .T. ) ;
#19169=CIRCLE ( 'NONE', #20595, 6.728125000000022560 ) ;
#19206=CARTESIAN_POINT ( 'NONE',  ( 1.500000000000001332, 6.678152076600409922E-16, -5.453125000000000000 ) ) ;
#19215=CYLINDRICAL_SURFACE ( 'NONE', #1384, 6.728125000000022560 ) ;
#19280=CARTESIAN_POINT ( 'NONE',  ( 1.199999999999992628, 8.434754829127421589E-16, 6.887500000000022382 ) ) ;
#19285=ORIENTED_EDGE ( 'NONE', *, *, #12658, .F. ) ;
#19294=CARTESIAN_POINT ( 'NONE',  ( -1.114300000000000290, 8.409404640385035208E-16, 6.866799999999992465 ) ) ;
#19314=EDGE_CURVE ( 'NONE', #14440, #17955, #14432, .T. ) ;
#19325=AXIS2_PLACEMENT_3D ( 'NONE', #19383, #11086, #4246 ) ;
#19326=CARTESIAN_POINT ( 'NONE',  ( 1.114299999999999846, 0.000000000000000000, 0.000000000000000000 ) ) ;
#19330=LINE ( 'NONE', #5861, #5525 ) ;
#19349=ADVANCED_FACE ( 'NONE', ( #20409 ), #7249, .F. ) ;
#19367=AXIS2_PLACEMENT_3D ( 'NONE', #14014, #20336, #539 ) ;
#19383=CARTESIAN_POINT ( 'NONE',  ( 1.139999999999995239, 0.000000000000000000, 0.000000000000000000 ) ) ;
#19392=DIRECTION ( 'NONE',  ( 0.000000000000000000, 0.000000000000000000, -1.000000000000000000 ) ) ;
#19443=ORIENTED_EDGE ( 'NONE', *, *, #11741, .F. ) ;
#19497=EDGE_LOOP ( 'NONE', ( #9763, #18824, #16981, #12849 ) ) ;
#19509=AXIS2_PLACEMENT_3D ( 'NONE', #5518, #12248, #14127 ) ;
#19536=DIRECTION ( 'NONE',  ( 0.000000000000000000, 0.000000000000000000, -1.000000000000000000 ) ) ;
#19543=VERTEX_POINT ( 'NONE', #19280 ) ;
#19546=ORIENTED_EDGE ( 'NONE', *, *, #17717, .F. ) ;
#19567=CONICAL_SURFACE ( 'NONE', #10044, 5.453125000000000000, 0.4883339510564123076 ) ;
#19621=DIRECTION ( 'NONE',  ( 0.000000000000000000, 0.000000000000000000, -1.000000000000000000 ) ) ;
#19627=EDGE_CURVE ( 'NONE', #4382, #16727, #8304, .T. ) ;
#19641=DIRECTION ( 'NONE',  ( -1.000000000000000000, 0.000000000000000000, -0.000000000000000000 ) ) ;
#19671=CARTESIAN_POINT ( 'NONE',  ( -90.00000000000000000, 0.000000000000000000, 0.000000000000000000 ) ) ;
#19688=ORIENTED_EDGE ( 'NONE', *, *, #15811, .T. ) ;
#19714=AXIS2_PLACEMENT_3D ( 'NONE', #13693, #1983, #5630 ) ;
#19744=ORIENTED_EDGE ( 'NONE', *, *, #17699, .T. ) ;
#19749=LINE ( 'NONE', #14443, #5958 ) ;
#19752=EDGE_CURVE ( 'NONE', #21211, #14549, #14300, .T. ) ;
#19785=CYLINDRICAL_SURFACE ( 'NONE', #11491, 6.728125000000023448 ) ;
#19798=ORIENTED_EDGE ( 'NONE', *, *, #21697, .F. ) ;
#19806=CARTESIAN_POINT ( 'NONE',  ( -1.200000000000006617, 0.000000000000000000, 0.000000000000000000 ) ) ;
#19815=ORIENTED_EDGE ( 'NONE', *, *, #13496, .F. ) ;
#19913=ORIENTED_EDGE ( 'NONE', *, *, #16209, .F. ) ;
#19916=CARTESIAN_POINT ( 'NONE',  ( -1.500000000000001332, 0.000000000000000000, 0.000000000000000000 ) ) ;
#19933=( NAMED_UNIT ( * ) PLANE_ANGLE_UNIT ( ) SI_UNIT ( $, .RADIAN. ) );
#19947=CARTESIAN_POINT ( 'NONE',  ( -90.00000000000000000, 8.239576745513313235E-16, 6.728125000000022560 ) ) ;
#19958=AXIS2_PLACEMENT_3D ( 'NONE', #15172, #14951, #13412 ) ;
#19969=EDGE_LOOP ( 'NONE', ( #2201, #5598 ) ) ;
#19980=AXIS2_PLACEMENT_3D ( 'NONE', #7780, #2247, #11193 ) ;
#19982=EDGE_CURVE ( 'NONE', #6262, #17309, #18202, .T. ) ;
#20038=AXIS2_PLACEMENT_3D ( 'NONE', #14143, #7197, #15481 ) ;
#20053=DIRECTION ( 'NONE',  ( 0.000000000000000000, 0.000000000000000000, 1.000000000000000000 ) ) ;
#20055=ORIENTED_EDGE ( 'NONE', *, *, #9365, .T. ) ;
#20056=DIRECTION ( 'NONE',  ( 0.000000000000000000, 0.000000000000000000, -1.000000000000000000 ) ) ;
#20098=DIRECTION ( 'NONE',  ( 0.000000000000000000, 0.000000000000000000, -1.000000000000000000 ) ) ;
#20151=ORIENTED_EDGE ( 'NONE', *, *, #957, .T. ) ;
#20172=DIRECTION ( 'NONE',  ( 0.000000000000000000, 0.000000000000000000, -1.000000000000000000 ) ) ;
#20187=DIRECTION ( 'NONE',  ( 0.000000000000000000, 0.000000000000000000, 1.000000000000000000 ) ) ;
#20240=CARTESIAN_POINT ( 'NONE',  ( -1.139999999999998570, 0.000000000000000000, -6.866799999999992465 ) ) ;
#20241=VERTEX_POINT ( 'NONE', #20240 ) ;
#20277=DIRECTION ( 'NONE',  ( 1.000000000000000000, 0.000000000000000000, 0.000000000000000000 ) ) ;
#20282=CARTESIAN_POINT ( 'NONE',  ( 1.500000000000001332, 8.239576745513314221E-16, 6.728125000000023448 ) ) ;
#20296=DIRECTION ( 'NONE',  ( 0.000000000000000000, 0.000000000000000000, -1.000000000000000000 ) ) ;
#20300=EDGE_CURVE ( 'NONE', #20799, #3466, #18679, .T. ) ;
#20323=CARTESIAN_POINT ( 'NONE',  ( -90.00000000000000000, 0.000000000000000000, 0.000000000000000000 ) ) ;
#20326=CLOSED_SHELL ( 'NONE', ( #16364, #10033, #19349, #40, #16428, #465, #20830, #18083, #10545, #8645, #17564, #17601, #10660, #8169, #6139, #14134, #12345, #11242, #955, #20420, #15025, #21661, #2842, #6811, #3135, #15151, #2656, #4643, #3761, #3546, #11500, #12414, #1485, #12292, #3735, #4519, #4191, #1809, #13536, #10597, #7804, #20465, #8254, #19160 ) ) ;
#20336=DIRECTION ( 'NONE',  ( -1.000000000000000000, 0.000000000000000000, 0.000000000000000000 ) ) ;
#20369=DIRECTION ( 'NONE',  ( 0.000000000000000000, 0.000000000000000000, -1.000000000000000000 ) ) ;
#20380=EDGE_LOOP ( 'NONE', ( #10775, #8863, #17202, #17003 ) ) ;
#20386=DIRECTION ( 'NONE',  ( 0.000000000000000000, 1.224646799147343593E-16, 1.000000000000000000 ) ) ;
#20388=FACE_OUTER_BOUND ( 'NONE', #1630, .T. ) ;
#20391=AXIS2_PLACEMENT_3D ( 'NONE', #10977, #2576, #11196 ) ;
#20395=FACE_OUTER_BOUND ( 'NONE', #12216, .T. ) ;
#20409=FACE_OUTER_BOUND ( 'NONE', #11208, .T. ) ;
#20420=ADVANCED_FACE ( 'NONE', ( #15982, #20855 ), #5721, .T. ) ;
#20431=EDGE_CURVE ( 'NONE', #13819, #16790, #12660, .T. ) ;
#20441=VECTOR ( 'NONE', #336, 1000.000000000000000 ) ;
#20448=ORIENTED_EDGE ( 'NONE', *, *, #6699, .F. ) ;
#20452=CARTESIAN_POINT ( 'NONE',  ( 1.199999999999992628, 0.000000000000000000, 0.000000000000000000 ) ) ;
#20463=ORIENTED_EDGE ( 'NONE', *, *, #1103, .F. ) ;
#20465=ADVANCED_FACE ( 'NONE', ( #17226 ), #8084, .T. ) ;
#20516=DIRECTION ( 'NONE',  ( 0.000000000000000000, 0.000000000000000000, -1.000000000000000000 ) ) ;
#20521=CARTESIAN_POINT ( 'NONE',  ( -90.00000000000000000, 0.000000000000000000, 0.000000000000000000 ) ) ;
#20527=PRODUCT_DEFINITION_FORMATION_WITH_SPECIFIED_SOURCE ( 'ANY', '', #9642, .NOT_KNOWN. ) ;
#20534=LINE ( 'NONE', #18766, #12582 ) ;
#20577=CARTESIAN_POINT ( 'NONE',  ( 1.399999999999999245, 0.000000000000000000, 0.000000000000000000 ) ) ;
#20595=AXIS2_PLACEMENT_3D ( 'NONE', #4570, #3227, #11302 ) ;
#20599=CARTESIAN_POINT ( 'NONE',  ( -90.00000000000000000, 0.000000000000000000, 0.000000000000000000 ) ) ;
#20622=EDGE_CURVE ( 'NONE', #13868, #17955, #2944, .T. ) ;
#20636=VERTEX_POINT ( 'NONE', #14979 ) ;
#20718=CIRCLE ( 'NONE', #8369, 6.866799999999992465 ) ;
#20721=EDGE_CURVE ( 'NONE', #18882, #9461, #5368, .T. ) ;
#20736=DIRECTION ( 'NONE',  ( 1.000000000000000000, 0.000000000000000000, 0.000000000000000000 ) ) ;
#20750=EDGE_LOOP ( 'NONE', ( #19015, #11885, #14385, #8801 ) ) ;
#20794=VECTOR ( 'NONE', #7462, 1000.000000000000000 ) ;
#20799=VERTEX_POINT ( 'NONE', #7037 ) ;
#20830=ADVANCED_FACE ( 'NONE', ( #2156 ), #15629, .T. ) ;
#20843=CARTESIAN_POINT ( 'NONE',  ( -1.129531546211690385, 8.434754829127421589E-16, 6.887500000000022382 ) ) ;
#20855=FACE_BOUND ( 'NONE', #14029, .T. ) ;
#20861=CARTESIAN_POINT ( 'NONE',  ( 1.500000000000001332, 6.775741118407465085E-16, -5.453125000000000000 ) ) ;
#20897=MANIFOLD_SOLID_BREP ( 'InnerRace', #20326 ) ;
#20907=DIRECTION ( 'NONE',  ( 0.000000000000000000, 0.000000000000000000, -1.000000000000000000 ) ) ;
#20911=CARTESIAN_POINT ( 'NONE',  ( -1.500000000000001332, 6.775741118407465085E-16, 5.453125000000000000 ) ) ;
#20924=CARTESIAN_POINT ( 'NONE',  ( 1.399999999999998579, 0.000000000000000000, 0.000000000000000000 ) ) ;
#20930=DIRECTION ( 'NONE',  ( 0.000000000000000000, 0.000000000000000000, -1.000000000000000000 ) ) ;
#20932=VERTEX_POINT ( 'NONE', #6790 ) ;
#20963=EDGE_LOOP ( 'NONE', ( #1117, #10656 ) ) ;
#20971=AXIS2_PLACEMENT_3D ( 'NONE', #7543, #5567, #9091 ) ;
#20974=DIRECTION ( 'NONE',  ( 0.000000000000000000, 1.000000000000000000, -1.224646799147353207E-16 ) ) ;
#20994=VERTEX_POINT ( 'NONE', #8120 ) ;
#21005=DIRECTION ( 'NONE',  ( 1.000000000000000000, -0.000000000000000000, -0.000000000000000000 ) ) ;
#21019=ORIENTED_EDGE ( 'NONE', *, *, #18765, .F. ) ;
#21020=DIRECTION ( 'NONE',  ( -0.000000000000000000, -1.000000000000000000, -0.000000000000000000 ) ) ;
#21053=DIRECTION ( 'NONE',  ( 0.000000000000000000, 0.000000000000000000, -1.000000000000000000 ) ) ;
#21062=CARTESIAN_POINT ( 'NONE',  ( 1.500000000000001332, 9.123618653647806797E-16, 7.400000000000020783 ) ) ;
#21073=CARTESIAN_POINT ( 'NONE',  ( -1.114300000000000068, 6.898680348956876061E-16, 5.633200000000004870 ) ) ;
#21080=ORIENTED_EDGE ( 'NONE', *, *, #6253, .F. ) ;
#21083=ORIENTED_EDGE ( 'NONE', *, *, #17441, .F. ) ;
#21088=CARTESIAN_POINT ( 'NONE',  ( 1.199999999999992628, 8.239576745513314221E-16, 6.728125000000023448 ) ) ;
#21096=TOROIDAL_SURFACE ( 'NONE', #21783, 7.400000000000019895, 0.1000000000000006994 ) ;
#21149=CARTESIAN_POINT ( 'NONE',  ( -1.399999999999999911, 0.000000000000000000, -5.100000000000000533 ) ) ;
#21160=ORIENTED_EDGE ( 'NONE', *, *, #9350, .F. ) ;
#21163=PRESENTATION_STYLE_ASSIGNMENT (( #14410 ) ) ;
#21211=VERTEX_POINT ( 'NONE', #17814 ) ;
#21224=FACE_BOUND ( 'NONE', #15576, .T. ) ;
#21234=CARTESIAN_POINT ( 'NONE',  ( -1.139999999999998570, 0.000000000000000000, 0.000000000000000000 ) ) ;
#21287=ORIENTED_EDGE ( 'NONE', *, *, #8576, .T. ) ;
#21313=CIRCLE ( 'NONE', #11799, 5.453125000000000000 ) ;
#21317=ORIENTED_EDGE ( 'NONE', *, *, #6024, .T. ) ;
#21321=LINE ( 'NONE', #9705, #11724 ) ;
#21325=DIRECTION ( 'NONE',  ( -0.000000000000000000, 0.000000000000000000, 1.000000000000000000 ) ) ;
#21348=AXIS2_PLACEMENT_3D ( 'NONE', #14995, #16655, #6295 ) ;
#21408=VERTEX_POINT ( 'NONE', #4987 ) ;
#21436=AXIS2_PLACEMENT_3D ( 'NONE', #6738, #86, #12015 ) ;
#21447=AXIS2_PLACEMENT_3D ( 'NONE', #1567, #13605, #8099 ) ;
#21459=VERTEX_POINT ( 'NONE', #14928 ) ;
#21469=AXIS2_PLACEMENT_3D ( 'NONE', #3422, #8072, #16460 ) ;
#21483=ORIENTED_EDGE ( 'NONE', *, *, #14153, .F. ) ;
#21532=FACE_OUTER_BOUND ( 'NONE', #1738, .T. ) ;
#21547=FACE_OUTER_BOUND ( 'NONE', #11034, .T. ) ;
#21627=DIRECTION ( 'NONE',  ( 1.000000000000000000, 0.000000000000000000, 0.000000000000000000 ) ) ;
#21661=ADVANCED_FACE ( 'NONE', ( #668, #13214 ), #14445, .T. ) ;
#21662=VECTOR ( 'NONE', #3149, 1000.000000000000000 ) ;
#21686=AXIS2_PLACEMENT_3D ( 'NONE', #10831, #7201, #772 ) ;
#21697=EDGE_CURVE ( 'NONE', #11959, #21408, #2844, .T. ) ;
#21705=AXIS2_PLACEMENT_3D ( 'NONE', #16989, #7375, #15760 ) ;
#21735=LINE ( 'NONE', #4840, #11460 ) ;
#21741=AXIS2_PLACEMENT_3D ( 'NONE', #6174, #1004, #14892 ) ;
#21783=AXIS2_PLACEMENT_3D ( 'NONE', #3187, #16661, #13561 ) ;
#21815=FACE_OUTER_BOUND ( 'NONE', #7805, .T. ) ;
#21822=CARTESIAN_POINT ( 'NONE',  ( -1.400000000000000577, 9.062386313690438040E-16, 7.400000000000019895 ) ) ;
#21825=CYLINDRICAL_SURFACE ( 'NONE', #11690, 6.728125000000023448 ) ;
#21826=EDGE_LOOP ( 'NONE', ( #3933, #8357 ) ) ;
#21837=CARTESIAN_POINT ( 'NONE',  ( 0.000000000000000000, 0.000000000000000000, 0.000000000000000000 ) ) ;
ENDSEC;
END-ISO-10303-21;
